ISO-10303-21;
HEADER;
FILE_DESCRIPTION (('STEP AP214'),
    '1' );
FILE_NAME ('hex flange nut gradea_iso_ISO - 4161 - M5 - N.step',
    '2026-10-08T13:46:47',
    ( '' ),
    ( '' ),
    'SwSTEP 2.0',
    'SolidWorks 2026',
    '' );
FILE_SCHEMA (( 'AUTOMOTIVE_DESIGN' ));
ENDSEC;

DATA;
#2=CARTESIAN_POINT ( 'NONE',  ( -4.000000000000000000, 0.9868501483902560878, -0.09357334158579519445 ) ) ;
#38=DIRECTION ( 'NONE',  ( -0.000000000000000000, -0.000000000000000000, 1.000000000000000000 ) ) ;
#146=CARTESIAN_POINT ( 'NONE',  ( -4.197393957002303999, -0.8151795401431414234, -3.503767560748935139 ) ) ;
#169=DIRECTION ( 'NONE',  ( -1.000000000000000000, 0.000000000000000000, 0.000000000000000000 ) ) ;
#176=CARTESIAN_POINT ( 'NONE',  ( -1.317756351988340180, 3.857995168970202116, -0.04852650426601388955 ) ) ;
#208=CARTESIAN_POINT ( 'NONE',  ( 4.000000000000000000, -2.471525695159793035, -3.686886880705770864 ) ) ;
#211=CARTESIAN_POINT ( 'NONE',  ( -4.000000000000000000, -0.8232339106130515116, -3.430630286862743183 ) ) ;
#222=CARTESIAN_POINT ( 'NONE',  ( 4.000000000000000000, 2.309401076758497151, -3.433295621305379353 ) ) ;
#249=ORIENTED_EDGE ( 'NONE', *, *, #5499, .T. ) ;
#268=EDGE_LOOP ( 'NONE', ( #17451, #14337, #19038, #18297, #4703 ) ) ;
#276=FACE_OUTER_BOUND ( 'NONE', #8026, .T. ) ;
#282=ADVANCED_FACE ( 'NONE', ( #9074 ), #16365, .T. ) ;
#286=DIRECTION ( 'NONE',  ( 0.000000000000000000, 0.000000000000000000, -1.000000000000000000 ) ) ;
#298=CARTESIAN_POINT ( 'NONE',  ( -2.500000000000000444, 3.061616997868383634E-16, -5.000000000000000888 ) ) ;
#305=B_SPLINE_CURVE_WITH_KNOTS ( 'NONE', 3,
 ( #22141, #7915, #17258, #22261, #2503 ),
 .UNSPECIFIED., .F., .F.,
 ( 4, 1, 4 ),
 ( 0.000000000000000000, 0.002309401076758506657, 0.004618802153517013315 ),
 .UNSPECIFIED. ) ;
#334=CARTESIAN_POINT ( 'NONE',  ( -4.211399284164270895, 2.459729995988205964, -3.751162237960538715 ) ) ;
#344=ORIENTED_EDGE ( 'NONE', *, *, #2171, .T. ) ;
#377=ORIENTED_EDGE ( 'NONE', *, *, #743, .F. ) ;
#408=ORIENTED_EDGE ( 'NONE', *, *, #13246, .T. ) ;
#439=PRODUCT_DEFINITION_CONTEXT ( 'detailed design', #1495, 'design' ) ;
#446=ORIENTED_EDGE ( 'NONE', *, *, #4266, .T. ) ;
#457=CARTESIAN_POINT ( 'NONE',  ( 4.204115023516791005, -1.660442669500199919, -3.602151381774560068 ) ) ;
#459=CARTESIAN_POINT ( 'NONE',  ( -4.000000000000000000, 2.511478553582031203, -3.469254451724764543 ) ) ;
#540=CARTESIAN_POINT ( 'NONE',  ( -0.5276280594146446346, 4.314175951381965746, -3.320322319201721495 ) ) ;
#550=CARTESIAN_POINT ( 'NONE',  ( 3.522875095019493141, -2.820352903225631369, -3.598441714920572299 ) ) ;
#632=DIRECTION ( 'NONE',  ( 1.000000000000000000, 0.000000000000000000, 0.000000000000000000 ) ) ;
#648=CARTESIAN_POINT ( 'NONE',  ( -1.655952806101422814, 3.662737355149034979, -7.623296525288699970E-18 ) ) ;
#656=CARTESIAN_POINT ( 'NONE',  ( -2.712762565639006418, 3.052587955997511759, -3.430618716626627318 ) ) ;
#713=DIRECTION ( 'NONE',  ( -0.000000000000000000, -0.000000000000000000, 1.000000000000000000 ) ) ;
#721=ADVANCED_FACE ( 'NONE', ( #14507 ), #11026, .T. ) ;
#743=EDGE_CURVE ( 'NONE', #7467, #16789, #1892, .T. ) ;
#797=VECTOR ( 'NONE', #16186, 1000.000000000000227 ) ;
#818=EDGE_LOOP ( 'NONE', ( #23139, #22622, #21693, #4272 ) ) ;
#852=ADVANCED_FACE ( 'NONE', ( #10150 ), #10485, .T. ) ;
#880=DIRECTION ( 'NONE',  ( 0.000000000000000000, 0.000000000000000000, 1.000000000000000000 ) ) ;
#904=EDGE_CURVE ( 'NONE', #21943, #17013, #4123, .T. ) ;
#946=VERTEX_POINT ( 'NONE', #13176 ) ;
#971=AXIS2_PLACEMENT_3D ( 'NONE', #12093, #6451, #13770 ) ;
#978=B_SPLINE_CURVE_WITH_KNOTS ( 'NONE', 3,
 ( #7008, #16230, #8938, #21585, #12539, #19802 ),
 .UNSPECIFIED., .F., .F.,
 ( 4, 2, 4 ),
 ( 0.003358874760055550156, 0.004541967308452096383, 0.005725059856848641743 ),
 .UNSPECIFIED. ) ;
#1007=DIRECTION ( 'NONE',  ( 0.000000000000000000, 0.000000000000000000, 1.000000000000000000 ) ) ;
#1022=CARTESIAN_POINT ( 'NONE',  ( -0.1756481739660520902, 4.720212674038980261, -3.469390959564065291 ) ) ;
#1033=CONICAL_SURFACE ( 'NONE', #4476, 4.000000000000000000, 0.8911886515913786111 ) ;
#1038=FACE_OUTER_BOUND ( 'NONE', #18547, .T. ) ;
#1082=CARTESIAN_POINT ( 'NONE',  ( -4.211140560182196957, 2.431303136016537803, -3.745885042887433514 ) ) ;
#1098=FILL_AREA_STYLE ('',( #14054 ) ) ;
#1103=AXIS2_PLACEMENT_3D ( 'NONE', #15008, #22627, #5874 ) ;
#1152=CARTESIAN_POINT ( 'NONE',  ( 0.000000000000000000, 0.000000000000000000, -4.000000000000000000 ) ) ;
#1171=CARTESIAN_POINT ( 'NONE',  ( -2.855764796983342624, 2.970025579236414082, -0.09382832055445475272 ) ) ;
#1173=EDGE_CURVE ( 'NONE', #1978, #6221, #8576, .T. ) ;
#1234=( NAMED_UNIT ( * ) SI_UNIT ( $, .STERADIAN. ) SOLID_ANGLE_UNIT ( ) );
#1239=CARTESIAN_POINT ( 'NONE',  ( -3.472371940586054251, -2.614027278893156669, -3.320322319202162031 ) ) ;
#1261=EDGE_CURVE ( 'NONE', #20390, #10320, #978, .T. ) ;
#1273=CARTESIAN_POINT ( 'NONE',  ( 4.000000000000000000, 2.309401076758497151, -3.433295621305379353 ) ) ;
#1292=ORIENTED_EDGE ( 'NONE', *, *, #15053, .T. ) ;
#1299=CARTESIAN_POINT ( 'NONE',  ( 3.355112389629172576, -2.681727112203168950, -0.2256878752776777242 ) ) ;
#1350=AXIS2_PLACEMENT_3D ( 'NONE', #6037, #4242, #7493 ) ;
#1388=ORIENTED_EDGE ( 'NONE', *, *, #19640, .T. ) ;
#1397=ORIENTED_EDGE ( 'NONE', *, *, #16708, .T. ) ;
#1406=CIRCLE ( 'NONE', #7172, 0.5155456020628804703 ) ;
#1424=CARTESIAN_POINT ( 'NONE',  ( -4.000000000000000000, 0.000000000000000000, 0.000000000000000000 ) ) ;
#1429=EDGE_CURVE ( 'NONE', #8404, #10654, #11585, .T. ) ;
#1446=VECTOR ( 'NONE', #11096, 1000.000000000000000 ) ;
#1451=MECHANICAL_DESIGN_GEOMETRIC_PRESENTATION_REPRESENTATION('',(#20581),#7598);
#1454=CYLINDRICAL_SURFACE ( 'NONE', #22857, 2.500000000000000444 ) ;
#1480=CARTESIAN_POINT ( 'NONE',  ( -2.756197834950067094, -3.027510591568735254, -3.223146290109809797 ) ) ;
#1492=CARTESIAN_POINT ( 'NONE',  ( 0.000000000000000000, 0.000000000000000000, -4.000000000000000000 ) ) ;
#1495=APPLICATION_CONTEXT ( 'automotive_design' ) ;
#1535=AXIS2_PLACEMENT_3D ( 'NONE', #11276, #20220, #18550 ) ;
#1553=CARTESIAN_POINT ( 'NONE',  ( 5.560781378645573980, 6.809993116116507654E-16, -4.000000000000000000 ) ) ;
#1555=B_SPLINE_CURVE_WITH_KNOTS ( 'NONE', 3,
 ( #21035, #4761, #12096, #11981, #19248, #2836, #17596, #19361 ),
 .UNSPECIFIED., .F., .F.,
 ( 4, 2, 2, 4 ),
 ( 0.000000000000000000, 0.002450665683189819262, 0.003675998524784728893, 0.004901331366379639391 ),
 .UNSPECIFIED. ) ;
#1557=CARTESIAN_POINT ( 'NONE',  ( 0.000000000000000000, 0.000000000000000000, 0.000000000000000000 ) ) ;
#1599=DIRECTION ( 'NONE',  ( -0.000000000000000000, -0.000000000000000000, 1.000000000000000000 ) ) ;
#1639=ORIENTED_EDGE ( 'NONE', *, *, #904, .F. ) ;
#1666=EDGE_LOOP ( 'NONE', ( #4660, #14496, #2456, #7359 ) ) ;
#1672=PLANE ( 'NONE',  #19525 ) ;
#1708=CARTESIAN_POINT ( 'NONE',  ( 1.411581201560190495E-15, 4.862606272033091592, -3.745885042887436622 ) ) ;
#1712=VERTEX_POINT ( 'NONE', #6762 ) ;
#1723=CARTESIAN_POINT ( 'NONE',  ( 4.211140560182196957, 2.431303136016536470, -3.745885042887433514 ) ) ;
#1731=CONICAL_SURFACE ( 'NONE', #12098, 2.500000000000000888, 0.9599310885968785900 ) ;
#1771=CARTESIAN_POINT ( 'NONE',  ( 4.000000000000000000, 0.8378280264232961239, -3.220590601395640018 ) ) ;
#1834=LINE ( 'NONE', #9184, #13242 ) ;
#1838=CARTESIAN_POINT ( 'NONE',  ( -2.100000000000000089, 2.571758278209441957E-16, -5.000000000000000000 ) ) ;
#1863=ADVANCED_FACE ( 'NONE', ( #22044 ), #4904, .T. ) ;
#1865=ADVANCED_FACE ( 'NONE', ( #7723 ), #3867, .T. ) ;
#1890=CARTESIAN_POINT ( 'NONE',  ( 4.211405965630455661, 2.460463115436283932, -3.751298928144577882 ) ) ;
#1891=ORIENTED_EDGE ( 'NONE', *, *, #13776, .T. ) ;
#1892=LINE ( 'NONE', #7320, #4724 ) ;
#1899=CARTESIAN_POINT ( 'NONE',  ( 3.510273485745307731, 2.827716139362654424, -3.610536846335885564 ) ) ;
#1900=CIRCLE ( 'NONE', #14558, 4.000000000000000000 ) ;
#1903=CARTESIAN_POINT ( 'NONE',  ( 4.000000000000000000, -1.084202172485504434E-14, -3.142992957459231906 ) ) ;
#1951=CARTESIAN_POINT ( 'NONE',  ( -0.5636800770129166693, -4.293361309317430319, -3.531542292955206275 ) ) ;
#1976=CARTESIAN_POINT ( 'NONE',  ( -2.688821387764050996E-14, -4.618802153517012954, -0.4999999999999995559 ) ) ;
#1978=VERTEX_POINT ( 'NONE', #17404 ) ;
#1985=ORIENTED_EDGE ( 'NONE', *, *, #13640, .F. ) ;
#1999=CARTESIAN_POINT ( 'NONE',  ( 4.000000000000000000, -1.677850389431204459, -3.535268758346977513 ) ) ;
#2003=DIRECTION ( 'NONE',  ( -1.000000000000000000, 0.000000000000000000, 0.000000000000000000 ) ) ;
#2007=CARTESIAN_POINT ( 'NONE',  ( -4.000000000000000888, -1.539600717839011201, -3.300726591567081591 ) ) ;
#2009=CARTESIAN_POINT ( 'NONE',  ( 3.861362476283255685, 2.629030857715988656, -3.671615880910370500 ) ) ;
#2011=ORIENTED_EDGE ( 'NONE', *, *, #18486, .F. ) ;
#2018=CARTESIAN_POINT ( 'NONE',  ( 0.000000000000000000, 0.000000000000000000, 0.000000000000000000 ) ) ;
#2054=DIRECTION ( 'NONE',  ( 0.5000000000000022204, 0.8660254037844374864, -0.000000000000000000 ) ) ;
#2129=CARTESIAN_POINT ( 'NONE',  ( 1.391697335622810172, 4.043246145443375461, -3.503898532754365913 ) ) ;
#2158=SHAPE_DEFINITION_REPRESENTATION ( #4559, #15757 ) ;
#2159=ORIENTED_EDGE ( 'NONE', *, *, #13788, .F. ) ;
#2171=EDGE_CURVE ( 'NONE', #21411, #21943, #12691, .T. ) ;
#2247=CARTESIAN_POINT ( 'NONE',  ( -4.000000000000000000, -1.680117682357936904, -3.316611593218794951 ) ) ;
#2283=CARTESIAN_POINT ( 'NONE',  ( 0.000000000000000000, 0.000000000000000000, 0.000000000000000000 ) ) ;
#2315=CARTESIAN_POINT ( 'NONE',  ( 0.02511973781850649831, -4.877415612947427981, -3.751298745799844792 ) ) ;
#2325=ORIENTED_EDGE ( 'NONE', *, *, #15515, .F. ) ;
#2368=CARTESIAN_POINT ( 'NONE',  ( -3.999999999998910649, -1.658469974638591804, -3.531532913075256186 ) ) ;
#2405=PRODUCT_CONTEXT ( 'NONE', #10237, 'mechanical' ) ;
#2412=AXIS2_PLACEMENT_3D ( 'NONE', #20205, #21999, #18423 ) ;
#2421=CARTESIAN_POINT ( 'NONE',  ( -3.974344831685191280E-13, 4.796734841935104576, -3.721909803043223608 ) ) ;
#2456=ORIENTED_EDGE ( 'NONE', *, *, #10434, .F. ) ;
#2460=CARTESIAN_POINT ( 'NONE',  ( 3.436319922986518449, -2.634841920959471562, -3.531542292954761741 ) ) ;
#2501=EDGE_CURVE ( 'NONE', #946, #5741, #9719, .T. ) ;
#2502=CONICAL_SURFACE ( 'NONE', #1350, 4.000000000000000000, 0.8911886515913786111 ) ;
#2503=CARTESIAN_POINT ( 'NONE',  ( -4.000000000000000000, 2.309401076758498483, -3.433295621305379353 ) ) ;
#2584=VERTEX_POINT ( 'NONE', #23099 ) ;
#2596=PLANE ( 'NONE',  #8049 ) ;
#2625=DIRECTION ( 'NONE',  ( 1.000000000000000000, 0.000000000000000000, 0.000000000000000000 ) ) ;
#2630=ADVANCED_FACE ( 'NONE', ( #3687 ), #3926, .F. ) ;
#2699=B_SPLINE_CURVE_WITH_KNOTS ( 'NONE', 3,
 ( #3230, #8759, #8532, #6961, #14278, #21539 ),
 .UNSPECIFIED., .F., .F.,
 ( 4, 2, 4 ),
 ( -3.640115492410698714E-06, 0.0002066546034006521879, 0.0004169493222937151081 ),
 .UNSPECIFIED. ) ;
#2720=ORIENTED_EDGE ( 'NONE', *, *, #16977, .T. ) ;
#2727=CARTESIAN_POINT ( 'NONE',  ( 1.828356344711641102, 3.563200125723180900, -5.433716356636336675E-16 ) ) ;
#2762=ADVANCED_FACE ( 'NONE', ( #11152 ), #15048, .T. ) ;
#2792=CARTESIAN_POINT ( 'NONE',  ( 5.384454397937118664, 0.000000000000000000, -4.484454397937119197 ) ) ;
#2807=FILL_AREA_STYLE ('',( #17323 ) ) ;
#2812=CARTESIAN_POINT ( 'NONE',  ( 4.000000000000000000, -1.942223658245635809, -0.3516579909967643691 ) ) ;
#2816=CARTESIAN_POINT ( 'NONE',  ( -0.6448876103708541807, -4.246476118072358474, -0.2256878752776773356 ) ) ;
#2836=CARTESIAN_POINT ( 'NONE',  ( 0.6937372685066666156, -4.453844082567737672, -3.610536846335894445 ) ) ;
#2880=CARTESIAN_POINT ( 'NONE',  ( 0.000000000000000000, 0.000000000000000000, -0.2800830152838844622 ) ) ;
#2894=VECTOR ( 'NONE', #5148, 1000.000000000000000 ) ;
#2895=B_SPLINE_CURVE_WITH_KNOTS ( 'NONE', 3,
 ( #11448, #7955, #9521, #7483, #14800 ),
 .UNSPECIFIED., .F., .F.,
 ( 4, 1, 4 ),
 ( 0.000000000000000000, 0.002309401076758505356, 0.004618802153517010713 ),
 .UNSPECIFIED. ) ;
#2920=CARTESIAN_POINT ( 'NONE',  ( 4.024499207728657879, -2.323545700935587988, -3.572172305156509964 ) ) ;
#2928=CARTESIAN_POINT ( 'NONE',  ( -1.312671235360383548, -3.860931062424228788, -0.05923475698271369466 ) ) ;
#2929=VECTOR ( 'NONE', #5199, 1000.000000000000114 ) ;
#2969=AXIS2_PLACEMENT_3D ( 'NONE', #9767, #13600, #22670 ) ;
#2978=DIRECTION ( 'NONE',  ( -1.000000000000000000, 0.000000000000000000, 0.000000000000000000 ) ) ;
#2980=CARTESIAN_POINT ( 'NONE',  ( -2.000000000000007550, -3.464101615137749945, 0.000000000000000000 ) ) ;
#3015=( NAMED_UNIT ( * ) SI_UNIT ( $, .STERADIAN. ) SOLID_ANGLE_UNIT ( ) );
#3049=ORIENTED_EDGE ( 'NONE', *, *, #10074, .F. ) ;
#3094=CARTESIAN_POINT ( 'NONE',  ( -0.6666666666666666297, -4.233901974057276973, -3.300726591567087365 ) ) ;
#3111=CARTESIAN_POINT ( 'NONE',  ( 0.000000000000000000, 0.000000000000000000, 0.000000000000000000 ) ) ;
#3115=CARTESIAN_POINT ( 'NONE',  ( 3.680118525130245732, -2.494084732383344605, -0.3507732604232533524 ) ) ;
#3127=CARTESIAN_POINT ( 'NONE',  ( -2.682243648011671588, -3.070208061305317759, -0.04852650426602272971 ) ) ;
#3173=CARTESIAN_POINT ( 'NONE',  ( 0.5449313310647804220, 4.304185902836899835, -3.316620875263383894 ) ) ;
#3189=ORIENTED_EDGE ( 'NONE', *, *, #20301, .T. ) ;
#3209=PLANE ( 'NONE',  #14907 ) ;
#3224=CARTESIAN_POINT ( 'NONE',  ( 0.000000000000000000, 0.000000000000000000, 0.000000000000000000 ) ) ;
#3230=CARTESIAN_POINT ( 'NONE',  ( -4.211140560182196957, 2.431303136016537803, -3.745885042887433514 ) ) ;
#3296=FACE_OUTER_BOUND ( 'NONE', #11836, .T. ) ;
#3330=CARTESIAN_POINT ( 'NONE',  ( -4.211140560182196957, 2.431303136016537803, -3.745885042887433514 ) ) ;
#3356=CARTESIAN_POINT ( 'NONE',  ( -4.000000000000000000, 2.309401076758498483, -0.4999999999999927280 ) ) ;
#3360=DIRECTION ( 'NONE',  ( -1.000000000000000000, 0.000000000000000000, 0.000000000000000000 ) ) ;
#3423=CARTESIAN_POINT ( 'NONE',  ( 3.999999999999999112, 1.941961291383486277, -0.3515519931180248192 ) ) ;
#3448=EDGE_CURVE ( 'NONE', #10320, #23289, #12456, .T. ) ;
#3476=EDGE_CURVE ( 'NONE', #14331, #20947, #21394, .T. ) ;
#3496=VERTEX_POINT ( 'NONE', #19747 ) ;
#3558=AXIS2_PLACEMENT_3D ( 'NONE', #20770, #11712, #9456 ) ;
#3566=ORIENTED_EDGE ( 'NONE', *, *, #15515, .T. ) ;
#3596=CARTESIAN_POINT ( 'NONE',  ( -6.259644161404860030E-16, -4.618802153517027165, -3.433295621305388234 ) ) ;
#3611=EDGE_LOOP ( 'NONE', ( #1388, #11614, #16915 ) ) ;
#3649=CARTESIAN_POINT ( 'NONE',  ( 1.567478505476134606E-15, 4.618802153517012066, -5.000000000000000000 ) ) ;
#3662=EDGE_CURVE ( 'NONE', #22700, #7989, #4277, .T. ) ;
#3687=FACE_OUTER_BOUND ( 'NONE', #17622, .T. ) ;
#3689=EDGE_CURVE ( 'NONE', #23683, #8317, #6280, .T. ) ;
#3691=CARTESIAN_POINT ( 'NONE',  ( -4.000000000000000000, 2.309401076758498483, -3.433295621305379353 ) ) ;
#3723=ORIENTED_EDGE ( 'NONE', *, *, #13353, .F. ) ;
#3738=VECTOR ( 'NONE', #12191, 1000.000000000000000 ) ;
#3752=AXIS2_PLACEMENT_3D ( 'NONE', #14729, #18295, #19609 ) ;
#3775=ORIENTED_EDGE ( 'NONE', *, *, #1173, .T. ) ;
#3812=FACE_OUTER_BOUND ( 'NONE', #21687, .T. ) ;
#3818=AXIS2_PLACEMENT_3D ( 'NONE', #10655, #12092, #23434 ) ;
#3833=ORIENTED_EDGE ( 'NONE', *, *, #20301, .F. ) ;
#3835=EDGE_CURVE ( 'NONE', #21424, #20390, #19139, .T. ) ;
#3844=B_SPLINE_CURVE_WITH_KNOTS ( 'NONE', 3,
 ( #12953, #20095, #1903, #9245, #222 ),
 .UNSPECIFIED., .F., .F.,
 ( 4, 1, 4 ),
 ( 0.000000000000000000, 0.002309401076758505790, 0.004618802153517011580 ),
 .UNSPECIFIED. ) ;
#3867=PLANE ( 'NONE',  #18289 ) ;
#3925=CARTESIAN_POINT ( 'NONE',  ( -4.203934362469166963, -1.640673743454851286, -3.598432614606932756 ) ) ;
#3926=CYLINDRICAL_SURFACE ( 'NONE', #3950, 2.100000000000000089 ) ;
#3936=CARTESIAN_POINT ( 'NONE',  ( 4.000000000000000000, 2.309401076758515803, -0.4999999999999995559 ) ) ;
#3950=AXIS2_PLACEMENT_3D ( 'NONE', #9346, #7322, #14862 ) ;
#4006=CARTESIAN_POINT ( 'NONE',  ( 0.000000000000000000, 0.000000000000000000, 0.000000000000000000 ) ) ;
#4045=DIRECTION ( 'NONE',  ( -0.000000000000000000, -0.000000000000000000, 1.000000000000000000 ) ) ;
#4046=LINE ( 'NONE', #20437, #19310 ) ;
#4057=DIRECTION ( 'NONE',  ( -0.000000000000000000, -0.000000000000000000, 1.000000000000000000 ) ) ;
#4083=ORIENTED_EDGE ( 'NONE', *, *, #13845, .F. ) ;
#4088=ORIENTED_EDGE ( 'NONE', *, *, #4824, .F. ) ;
#4100=ADVANCED_FACE ( 'NONE', ( #21994 ), #22726, .F. ) ;
#4104=AXIS2_PLACEMENT_3D ( 'NONE', #2018, #18680, #4188 ) ;
#4106=CARTESIAN_POINT ( 'NONE',  ( 2.548804901056335857E-15, 4.736522675502163437, -3.681124513963624612 ) ) ;
#4123=B_SPLINE_CURVE_WITH_KNOTS ( 'NONE', 3,
 ( #4735, #15543, #2920, #11953, #18534, #22808 ),
 .UNSPECIFIED., .F., .F.,
 ( 4, 2, 4 ),
 ( 4.336808689942017736E-19, 0.0002095117440854729585, 0.0004190234881709454834 ),
 .UNSPECIFIED. ) ;
#4140=CARTESIAN_POINT ( 'NONE',  ( 4.000000000000000000, -1.560351142792952617, -0.2242961665059816367 ) ) ;
#4143=EDGE_LOOP ( 'NONE', ( #18603, #5082, #17062, #10040 ) ) ;
#4180=PRODUCT_DEFINITION_FORMATION_WITH_SPECIFIED_SOURCE ( 'ANY', '', #15290, .NOT_KNOWN. ) ;
#4188=DIRECTION ( 'NONE',  ( 1.000000000000000000, 0.000000000000000000, 0.000000000000000000 ) ) ;
#4199=MECHANICAL_DESIGN_GEOMETRIC_PRESENTATION_REPRESENTATION('',(#6119),#7279);
#4242=DIRECTION ( 'NONE',  ( 0.000000000000000000, 0.000000000000000000, -1.000000000000000000 ) ) ;
#4264=CARTESIAN_POINT ( 'NONE',  ( -3.522875095019672109, 2.820352903225427532, -3.598441714920591394 ) ) ;
#4266=EDGE_CURVE ( 'NONE', #22700, #15024, #5423, .T. ) ;
#4272=ORIENTED_EDGE ( 'NONE', *, *, #22533, .F. ) ;
#4273=CARTESIAN_POINT ( 'NONE',  ( 1.243802165048773611, -3.900692638707475624, -3.223146290109810241 ) ) ;
#4277=B_SPLINE_CURVE_WITH_KNOTS ( 'NONE', 3,
 ( #18430, #22007, #2129, #5618, #20568, #1899, #2009, #9464 ),
 .UNSPECIFIED., .F., .F.,
 ( 4, 2, 2, 4 ),
 ( 7.780516681398759253E-20, 0.002450665683189819696, 0.003675998524784729327, 0.004901331366379639391 ),
 .UNSPECIFIED. ) ;
#4283=B_SPLINE_CURVE_WITH_KNOTS ( 'NONE', 3,
 ( #3330, #9227, #7421, #14617, #5605, #12593, #20195, #10674 ),
 .UNSPECIFIED., .F., .F.,
 ( 4, 2, 2, 4 ),
 ( 0.000000000000000000, 0.002450665683189820997, 0.003675998524784731495, 0.004901331366379641993 ),
 .UNSPECIFIED. ) ;
#4309=EDGE_LOOP ( 'NONE', ( #377, #15317, #1292, #15349, #4884 ) ) ;
#4335=EDGE_CURVE ( 'NONE', #8665, #2584, #13235, .T. ) ;
#4377=CARTESIAN_POINT ( 'NONE',  ( -3.436319922987618902, 2.634841920961291439, -3.531542292955721862 ) ) ;
#4383=CARTESIAN_POINT ( 'NONE',  ( -2.688821387764050996E-14, -4.618802153517012954, -0.4999999999999995559 ) ) ;
#4411=AXIS2_PLACEMENT_3D ( 'NONE', #3224, #14153, #12484 ) ;
#4461=EDGE_LOOP ( 'NONE', ( #9468, #19930, #6064, #6579, #12750 ) ) ;
#4476=AXIS2_PLACEMENT_3D ( 'NONE', #4006, #286, #169 ) ;
#4503=CARTESIAN_POINT ( 'NONE',  ( -0.1750025118121544265, -4.719839900820635314, -3.469254087858253399 ) ) ;
#4544=CARTESIAN_POINT ( 'NONE',  ( -2.000000000000006661, 3.464101615137750834, 0.000000000000000000 ) ) ;
#4559=PRODUCT_DEFINITION_SHAPE ( 'NONE', 'NONE',  #9760 ) ;
#4643=FACE_BOUND ( 'NONE', #15436, .T. ) ;
#4660=ORIENTED_EDGE ( 'NONE', *, *, #20365, .T. ) ;
#4703=ORIENTED_EDGE ( 'NONE', *, *, #10465, .T. ) ;
#4709=EDGE_LOOP ( 'NONE', ( #13314, #3189, #12036, #8234 ) ) ;
#4724=VECTOR ( 'NONE', #21885, 1000.000000000000000 ) ;
#4725=CARTESIAN_POINT ( 'NONE',  ( -4.204015924366189871, 1.626724848190922446, -3.610627190413390419 ) ) ;
#4735=CARTESIAN_POINT ( 'NONE',  ( 4.000000000000000000, -2.309401076758514915, -3.433295621305383349 ) ) ;
#4742=CARTESIAN_POINT ( 'NONE',  ( -1.828356344711647319, -3.563200125723192002, -1.076197711133951296E-14 ) ) ;
#4756=FACE_OUTER_BOUND ( 'NONE', #5320, .T. ) ;
#4759=B_SPLINE_CURVE_WITH_KNOTS ( 'NONE', 3,
 ( #6349, #10318, #19498, #1171, #13663, #15923, #20924, #4544 ),
 .UNSPECIFIED., .F., .F.,
 ( 4, 2, 2, 4 ),
 ( 2.465131517071352357E-07, 0.001183067374689843057, 0.001774477805458910071, 0.002365888236227977302 ),
 .UNSPECIFIED. ) ;
#4761=CARTESIAN_POINT ( 'NONE',  ( 3.511755186886750923, -2.826662030176382956, -3.597382984111582083 ) ) ;
#4780=CIRCLE ( 'NONE', #4411, 4.000000000000000000 ) ;
#4800=CARTESIAN_POINT ( 'NONE',  ( 0.000000000000000000, 0.000000000000000000, -5.000000000000000000 ) ) ;
#4820=SURFACE_SIDE_STYLE ('',( #20972 ) ) ;
#4824=EDGE_CURVE ( 'NONE', #8665, #1978, #21149, .T. ) ;
#4856=CARTESIAN_POINT ( 'NONE',  ( 2.100000000000000089, 0.000000000000000000, -5.000000000000000000 ) ) ;
#4858=CARTESIAN_POINT ( 'NONE',  ( 2.836893136758676270, 3.208949435745843903, -3.505054077164911241 ) ) ;
#4884=ORIENTED_EDGE ( 'NONE', *, *, #21029, .T. ) ;
#4904=TOROIDAL_SURFACE ( 'NONE', #15262, 5.384454397937118664, 0.5155456020628804703 ) ;
#4911=CONICAL_SURFACE ( 'NONE', #7987, 4.000000000000000000, 0.8911886515913786111 ) ;
#4928=FACE_BOUND ( 'NONE', #19113, .T. ) ;
#4936=CARTESIAN_POINT ( 'NONE',  ( 4.197393957002303999, 0.8151795401431359833, -3.503767560748935139 ) ) ;
#4983=ORIENTED_EDGE ( 'NONE', *, *, #8082, .T. ) ;
#4984=CARTESIAN_POINT ( 'NONE',  ( 4.235886605889389145, 2.417314728048528760, -3.751161874094018245 ) ) ;
#5006=ADVANCED_FACE ( 'NONE', ( #15212 ), #23528, .F. ) ;
#5042=CARTESIAN_POINT ( 'NONE',  ( -4.000000000000000000, 0.1981133338132459731, 2.096406544454392723E-17 ) ) ;
#5082=ORIENTED_EDGE ( 'NONE', *, *, #15357, .F. ) ;
#5148=DIRECTION ( 'NONE',  ( 0.000000000000000000, 0.000000000000000000, 1.000000000000000000 ) ) ;
#5155=ADVANCED_FACE ( 'NONE', ( #1038 ), #9805, .T. ) ;
#5199=DIRECTION ( 'NONE',  ( 0.8191520442889902442, 1.003171929053522651E-16, -0.5735764363510482688 ) ) ;
#5200=CARTESIAN_POINT ( 'NONE',  ( -1.390230914382372118, -4.043987460488664532, -3.502507215260523665 ) ) ;
#5214=CARTESIAN_POINT ( 'NONE',  ( 4.000000000000000888, 1.563622288139206118, -0.2253451193528334950 ) ) ;
#5217=CARTESIAN_POINT ( 'NONE',  ( 0.000000000000000000, 0.000000000000000000, -4.694516984716113228 ) ) ;
#5224=DIRECTION ( 'NONE',  ( -0.000000000000000000, -0.000000000000000000, 1.000000000000000000 ) ) ;
#5227=EDGE_CURVE ( 'NONE', #5741, #946, #12107, .T. ) ;
#5282=CARTESIAN_POINT ( 'NONE',  ( 4.211140560182196957, -2.431303136016555122, -3.745885042887436622 ) ) ;
#5304=CARTESIAN_POINT ( 'NONE',  ( -6.473970235329672780E-16, -4.862606272033106691, -3.745885042887442395 ) ) ;
#5320=EDGE_LOOP ( 'NONE', ( #11870, #15254, #9492, #14750 ) ) ;
#5330=ORIENTED_EDGE ( 'NONE', *, *, #13776, .F. ) ;
#5354=VERTEX_POINT ( 'NONE', #21741 ) ;
#5423=B_SPLINE_CURVE_WITH_KNOTS ( 'NONE', 3,
 ( #22176, #2421, #4106, #5909, #16816, #5791 ),
 .UNSPECIFIED., .F., .F.,
 ( 4, 2, 4 ),
 ( -3.640115492407174633E-06, 0.0002066546034006553863, 0.0004169493222937179812 ),
 .UNSPECIFIED. ) ;
#5432=ADVANCED_FACE ( 'NONE', ( #18758 ), #12922, .T. ) ;
#5466=DIRECTION ( 'NONE',  ( -1.000000000000000000, 0.000000000000000000, 0.000000000000000000 ) ) ;
#5491=CARTESIAN_POINT ( 'NONE',  ( 4.000000000000000000, 2.512223110932545023, -3.469391141908803711 ) ) ;
#5499=EDGE_CURVE ( 'NONE', #20947, #3496, #16894, .T. ) ;
#5500=CARTESIAN_POINT ( 'NONE',  ( -4.000000000000000000, -2.309401076758512694, -3.433295621305382461 ) ) ;
#5516=CARTESIAN_POINT ( 'NONE',  ( -3.264650091097280831E-13, -4.796980096169642493, -3.721999068284424617 ) ) ;
#5583=( BOUNDED_SURFACE ( )  B_SPLINE_SURFACE ( 3, 2, ( 
 ( #4503, #10048, #17336 ),
 ( #11723, #8127, #9567 ),
 ( #4273, #8239, #18876 ),
 ( #5830, #7762, #17219 ),
 ( #15437, #2460, #550 ),
 ( #22592, #7999, #13630 ) ),
 .UNSPECIFIED., .F., .F., .F. ) 
 B_SPLINE_SURFACE_WITH_KNOTS ( ( 4, 2, 4 ),
 ( 3, 3 ),
 ( 0.02032853247518126918, 0.02278863295364821906, 0.02524873343211517240 ),
 ( 0.000000000000000000, 1.000000000000000000 ),
 .UNSPECIFIED. ) 
 GEOMETRIC_REPRESENTATION_ITEM ( )  RATIONAL_B_SPLINE_SURFACE ( (
 ( 1.000000000000000000, 0.8047781615896837382, 1.000000000000000000),
 ( 1.000000000000000000, 0.8123767586289252218, 1.000000000000000000),
 ( 1.000000000000000000, 0.8190662415564388121, 1.000000000000000000),
 ( 1.000000000000000000, 0.8192361015669026303, 1.000000000000000000),
 ( 1.000000000000000000, 0.8126135807103900266, 1.000000000000000000),
 ( 1.000000000000000000, 0.8047712338318593339, 1.000000000000000000) ) ) 
 REPRESENTATION_ITEM ( '' )  SURFACE ( )  );
#5588=ORIENTED_EDGE ( 'NONE', *, *, #17587, .T. ) ;
#5597=B_SPLINE_CURVE_WITH_KNOTS ( 'NONE', 3,
 ( #23120, #19530, #3127, #10469, #6846, #21549 ),
 .UNSPECIFIED., .F., .F.,
 ( 4, 2, 4 ),
 ( 0.002365888236228001588, 0.003551327329835089319, 0.004736766423442177049 ),
 .UNSPECIFIED. ) ;
#5605=CARTESIAN_POINT ( 'NONE',  ( -1.393927851585477606, 4.043713361053528743, -3.526374918436835149 ) ) ;
#5610=CARTESIAN_POINT ( 'NONE',  ( 4.211399257449709665, -2.459727064652517114, -3.751161691472417736 ) ) ;
#5613=CARTESIAN_POINT ( 'NONE',  ( -4.000000000000000000, 1.677772373332757194, -3.535253723897187506 ) ) ;
#5618=CARTESIAN_POINT ( 'NONE',  ( 2.449848172108560096, 3.432307619358740514, -3.503702292528905637 ) ) ;
#5642=VERTEX_POINT ( 'NONE', #18199 ) ;
#5663=AXIS2_PLACEMENT_3D ( 'NONE', #1492, #8351, #10636 ) ;
#5741=VERTEX_POINT ( 'NONE', #18791 ) ;
#5744=CARTESIAN_POINT ( 'NONE',  ( 0.3198814748697593746, 4.434118497892183264, -0.3507732604232499107 ) ) ;
#5773=ORIENTED_EDGE ( 'NONE', *, *, #13640, .T. ) ;
#5791=CARTESIAN_POINT ( 'NONE',  ( 1.567478505476134606E-15, 4.618802153517012066, -3.433295621305382905 ) ) ;
#5830=CARTESIAN_POINT ( 'NONE',  ( 2.725741868436127202, -3.045094352033990148, -3.220599429844051453 ) ) ;
#5856=CARTESIAN_POINT ( 'NONE',  ( 1.654252653721905331, 3.663718938583014229, -0.01223254789873410957 ) ) ;
#5874=DIRECTION ( 'NONE',  ( -1.000000000000000000, 0.000000000000000000, 0.000000000000000000 ) ) ;
#5909=CARTESIAN_POINT ( 'NONE',  ( 2.290893957444128645E-15, 4.647089433458768681, -3.572167766733382877 ) ) ;
#5943=DIRECTION ( 'NONE',  ( 0.000000000000000000, 0.000000000000000000, -1.000000000000000000 ) ) ;
#5980=VERTEX_POINT ( 'NONE', #20913 ) ;
#5989=EDGE_CURVE ( 'NONE', #17013, #8404, #1555, .T. ) ;
#6037=CARTESIAN_POINT ( 'NONE',  ( 0.000000000000000000, 0.000000000000000000, 0.000000000000000000 ) ) ;
#6063=ORIENTED_EDGE ( 'NONE', *, *, #3662, .T. ) ;
#6064=ORIENTED_EDGE ( 'NONE', *, *, #743, .T. ) ;
#6119=STYLED_ITEM ( 'NONE', ( #19447 ), #22443 ) ;
#6193=ADVANCED_BREP_SHAPE_REPRESENTATION ( '', ( #22443, #7318 ), #16773 ) ;
#6197=UNCERTAINTY_MEASURE_WITH_UNIT (LENGTH_MEASURE( 1.000000000000000082E-05 ), #6630, 'distance_accuracy_value', 'NONE');
#6221=VERTEX_POINT ( 'NONE', #11000 ) ;
#6251=ORIENTED_EDGE ( 'NONE', *, *, #19640, .F. ) ;
#6280=B_SPLINE_CURVE_WITH_KNOTS ( 'NONE', 3,
 ( #22246, #5744, #7435, #14748, #13072, #5856, #2727, #17243 ),
 .UNSPECIFIED., .F., .F.,
 ( 4, 2, 2, 4 ),
 ( 2.465131517075058656E-07, 0.001183067374689851080, 0.001774477805458923299, 0.002365888236227995517 ),
 .UNSPECIFIED. ) ;
#6299=DIRECTION ( 'NONE',  ( -0.000000000000000000, -0.000000000000000000, 1.000000000000000000 ) ) ;
#6304=CARTESIAN_POINT ( 'NONE',  ( -1.257172072275743346, 3.892973519171203378, -3.433252694550776862 ) ) ;
#6349=CARTESIAN_POINT ( 'NONE',  ( -4.000000000000000000, 2.309401076758498483, -0.4999999999999927280 ) ) ;
#6396=B_SPLINE_CURVE_WITH_KNOTS ( 'NONE', 3,
 ( #19519, #11271, #7204, #16530, #9353, #3936 ),
 .UNSPECIFIED., .F., .F.,
 ( 4, 2, 4 ),
 ( 0.002365888236227995517, 0.003551327329835084114, 0.004736766423442172712 ),
 .UNSPECIFIED. ) ;
#6431=CARTESIAN_POINT ( 'NONE',  ( 1.287237434362044075, 3.875615274277557809, -3.430618716626812059 ) ) ;
#6451=DIRECTION ( 'NONE',  ( -0.000000000000000000, -0.000000000000000000, 1.000000000000000000 ) ) ;
#6457=EDGE_CURVE ( 'NONE', #3496, #7262, #22111, .T. ) ;
#6551=EDGE_LOOP ( 'NONE', ( #2325, #14864, #15138, #12605, #11231 ) ) ;
#6560=ORIENTED_EDGE ( 'NONE', *, *, #16708, .F. ) ;
#6579=ORIENTED_EDGE ( 'NONE', *, *, #13246, .F. ) ;
#6598=DIRECTION ( 'NONE',  ( -0.000000000000000000, -0.000000000000000000, 1.000000000000000000 ) ) ;
#6630=( LENGTH_UNIT ( ) NAMED_UNIT ( * ) SI_UNIT ( .MILLI., .METRE. ) );
#6663=EDGE_CURVE ( 'NONE', #8665, #1712, #22061, .T. ) ;
#6668=LINE ( 'NONE', #4856, #3738 ) ;
#6673=B_SPLINE_CURVE_WITH_KNOTS ( 'NONE', 3,
 ( #3596, #10936, #18215, #21908, #5516, #20232 ),
 .UNSPECIFIED., .F., .F.,
 ( 4, 2, 4 ),
 ( 0.000000000000000000, 0.0002095117440854740156, 0.0004190234881709480313 ),
 .UNSPECIFIED. ) ;
#6722=ORIENTED_EDGE ( 'NONE', *, *, #23292, .T. ) ;
#6757=CYLINDRICAL_SURFACE ( 'NONE', #20153, 2.100000000000000089 ) ;
#6762=CARTESIAN_POINT ( 'NONE',  ( -2.100000000000000089, 2.571758278209441957E-16, -0.2800830152838844622 ) ) ;
#6778=FACE_OUTER_BOUND ( 'NONE', #19870, .T. ) ;
#6780=CARTESIAN_POINT ( 'NONE',  ( 4.000000000000000000, -2.309401076758514915, -3.433295621305383349 ) ) ;
#6813=DIRECTION ( 'NONE',  ( -1.000000000000000000, 0.000000000000000000, 0.000000000000000000 ) ) ;
#6846=CARTESIAN_POINT ( 'NONE',  ( -3.679171394226034675, -2.494631558665844739, -0.3503314178412558211 ) ) ;
#6857=EDGE_LOOP ( 'NONE', ( #19280, #11379, #8017, #6560, #3049 ) ) ;
#6867=CIRCLE ( 'NONE', #1103, 2.500000000000000444 ) ;
#6905=CARTESIAN_POINT ( 'NONE',  ( 4.140404888673277384, 2.228338276487440428, -3.686887068327033390 ) ) ;
#6909=CARTESIAN_POINT ( 'NONE',  ( 4.000000000000000000, 0.7924765000094659007, -0.05906175389889852662 ) ) ;
#6936=CARTESIAN_POINT ( 'NONE',  ( -6.259644161404860030E-16, -4.618802153517027165, -3.433295621305388234 ) ) ;
#6943=DIRECTION ( 'NONE',  ( -1.000000000000000000, 0.000000000000000000, 0.000000000000000000 ) ) ;
#6955=DIRECTION ( 'NONE',  ( -0.000000000000000000, -0.000000000000000000, 1.000000000000000000 ) ) ;
#6961=CARTESIAN_POINT ( 'NONE',  ( -4.024497503033519941, 2.323544716729375459, -3.572167766733379768 ) ) ;
#7008=CARTESIAN_POINT ( 'NONE',  ( -4.000000000000000000, -2.309401076758515803, -0.4999999999999995559 ) ) ;
#7009=CARTESIAN_POINT ( 'NONE',  ( -1.274258131565027874, -3.883108878240886241, -3.220599429844051009 ) ) ;
#7084=CARTESIAN_POINT ( 'NONE',  ( -4.000000000000000000, 0.7924765000094600165, -0.05906175389889745803 ) ) ;
#7092=DIRECTION ( 'NONE',  ( 0.000000000000000000, 0.000000000000000000, -1.000000000000000000 ) ) ;
#7112=CIRCLE ( 'NONE', #7877, 5.560781378645573980 ) ;
#7141=( BOUNDED_SURFACE ( )  B_SPLINE_SURFACE ( 3, 2, ( 
 ( #22945, #6905, #4984 ),
 ( #11964, #15786, #8836 ),
 ( #22818, #15894, #4858 ),
 ( #8353, #6431, #17459 ),
 ( #3173, #23057, #19465 ),
 ( #1022, #10519, #17572 ) ),
 .UNSPECIFIED., .F., .F., .T. ) 
 B_SPLINE_SURFACE_WITH_KNOTS ( ( 4, 2, 4 ),
 ( 3, 3 ),
 ( 0.02032853247518126225, 0.02278863295364821212, 0.02524873343211516200 ),
 ( 0.000000000000000000, 1.000000000000000000 ),
 .UNSPECIFIED. ) 
 GEOMETRIC_REPRESENTATION_ITEM ( )  RATIONAL_B_SPLINE_SURFACE ( (
 ( 1.000000000000000000, 0.8047781615896835161, 1.000000000000000000),
 ( 1.000000000000000000, 0.8123767586291043008, 1.000000000000000000),
 ( 1.000000000000000000, 0.8190662415562011134, 1.000000000000000000),
 ( 1.000000000000000000, 0.8192361015671398849, 1.000000000000000000),
 ( 1.000000000000000000, 0.8126135807102121689, 1.000000000000000000),
 ( 1.000000000000000000, 0.8047712338318585568, 1.000000000000000000) ) ) 
 REPRESENTATION_ITEM ( '' )  SURFACE ( )  );
#7172=AXIS2_PLACEMENT_3D ( 'NONE', #2792, #20753, #18740 ) ;
#7204=CARTESIAN_POINT ( 'NONE',  ( 2.682243648011666703, 3.070208061305304881, -0.04852650426601266831 ) ) ;
#7210=CARTESIAN_POINT ( 'NONE',  ( -6.259644161404860030E-16, -4.618802153517027165, -5.000000000000000000 ) ) ;
#7233=DIRECTION ( 'NONE',  ( -0.000000000000000000, -0.000000000000000000, 1.000000000000000000 ) ) ;
#7262=VERTEX_POINT ( 'NONE', #2980 ) ;
#7277=ADVANCED_FACE ( 'NONE', ( #7679 ), #1454, .F. ) ;
#7279=( GEOMETRIC_REPRESENTATION_CONTEXT ( 3 ) GLOBAL_UNCERTAINTY_ASSIGNED_CONTEXT ( ( #19577 ) ) GLOBAL_UNIT_ASSIGNED_CONTEXT ( ( #22806, #8223, #1234 ) ) REPRESENTATION_CONTEXT ( 'NONE', 'WORKASPACE' ) );
#7287=( BOUNDED_SURFACE ( )  B_SPLINE_SURFACE ( 3, 2, ( 
 ( #17676, #19680, #10396 ),
 ( #1239, #10627, #17903 ),
 ( #1480, #8822, #23403 ),
 ( #7009, #14326, #5200 ),
 ( #16938, #1951, #18602 ),
 ( #14929, #16823, #2315 ) ),
 .UNSPECIFIED., .F., .F., .F. ) 
 B_SPLINE_SURFACE_WITH_KNOTS ( ( 4, 2, 4 ),
 ( 3, 3 ),
 ( 0.02032853247518126918, 0.02278863295364821906, 0.02524873343211516893 ),
 ( 0.000000000000000000, 1.000000000000000000 ),
 .UNSPECIFIED. ) 
 GEOMETRIC_REPRESENTATION_ITEM ( )  RATIONAL_B_SPLINE_SURFACE ( (
 ( 1.000000000000000000, 0.8047781615896838492, 1.000000000000000000),
 ( 1.000000000000000000, 0.8123767586288186404, 1.000000000000000000),
 ( 1.000000000000000000, 0.8190662415565814758, 1.000000000000000000),
 ( 1.000000000000000000, 0.8192361015667604107, 1.000000000000000000),
 ( 1.000000000000000000, 0.8126135807104967190, 1.000000000000000000),
 ( 1.000000000000000000, 0.8047712338318580017, 1.000000000000000000) ) ) 
 REPRESENTATION_ITEM ( '' )  SURFACE ( )  );
#7291=CIRCLE ( 'NONE', #13363, 2.100000000000000089 ) ;
#7318=AXIS2_PLACEMENT_3D ( 'NONE', #3111, #10686, #17843 ) ;
#7320=CARTESIAN_POINT ( 'NONE',  ( 4.000000000000000000, 2.309401076758497151, -5.000000000000000000 ) ) ;
#7322=DIRECTION ( 'NONE',  ( 0.000000000000000000, 0.000000000000000000, 1.000000000000000000 ) ) ;
#7333=CARTESIAN_POINT ( 'NONE',  ( -4.000000000000000888, 1.563622288139195238, -0.2253451193528307472 ) ) ;
#7359=ORIENTED_EDGE ( 'NONE', *, *, #8838, .F. ) ;
#7421=CARTESIAN_POINT ( 'NONE',  ( -2.805705207896067144, 3.226868319750155312, -3.503898532754364581 ) ) ;
#7428=CARTESIAN_POINT ( 'NONE',  ( 3.999999999999998224, 2.472263674411418588, -3.687027874309861897 ) ) ;
#7435=CARTESIAN_POINT ( 'NONE',  ( 0.6448876103708359731, 4.246476118072354922, -0.2256878752776725616 ) ) ;
#7444=DIRECTION ( 'NONE',  ( 0.000000000000000000, 0.000000000000000000, 1.000000000000000000 ) ) ;
#7467=VERTEX_POINT ( 'NONE', #1273 ) ;
#7473=TOROIDAL_SURFACE ( 'NONE', #18155, 5.384454397937118664, 0.5155456020628804703 ) ;
#7475=ADVANCED_FACE ( 'NONE', ( #10429 ), #16363, .F. ) ;
#7478=CARTESIAN_POINT ( 'NONE',  ( -4.197393957002303999, -7.773935952363655451E-14, -3.503767560748929810 ) ) ;
#7483=CARTESIAN_POINT ( 'NONE',  ( 0.6666666666666689611, 4.233901974057261874, -3.300726591567082480 ) ) ;
#7493=DIRECTION ( 'NONE',  ( -1.000000000000000000, 0.000000000000000000, 0.000000000000000000 ) ) ;
#7539=CARTESIAN_POINT ( 'NONE',  ( 4.000000000000000888, -0.8578082829538523635, -3.433262215449808696 ) ) ;
#7542=CARTESIAN_POINT ( 'NONE',  ( -4.197312064133472020, -0.8182229787990021874, -3.502518405183886685 ) ) ;
#7576=CIRCLE ( 'NONE', #23628, 4.000000000000000000 ) ;
#7598=( GEOMETRIC_REPRESENTATION_CONTEXT ( 3 ) GLOBAL_UNCERTAINTY_ASSIGNED_CONTEXT ( ( #6197 ) ) GLOBAL_UNIT_ASSIGNED_CONTEXT ( ( #6630, #19544, #12278 ) ) REPRESENTATION_CONTEXT ( 'NONE', 'WORKASPACE' ) );
#7611=DIRECTION ( 'NONE',  ( -0.000000000000000000, -0.000000000000000000, 1.000000000000000000 ) ) ;
#7668=CARTESIAN_POINT ( 'NONE',  ( -4.000000000000000000, -2.472261339043343220, -3.687027428081192326 ) ) ;
#7679=FACE_OUTER_BOUND ( 'NONE', #8704, .T. ) ;
#7723=FACE_OUTER_BOUND ( 'NONE', #4309, .T. ) ;
#7734=CARTESIAN_POINT ( 'NONE',  ( 0.000000000000000000, 0.000000000000000000, -5.000000000000000000 ) ) ;
#7755=CARTESIAN_POINT ( 'NONE',  ( 2.000000000000005329, -3.464101615137751722, 0.000000000000000000 ) ) ;
#7762=CARTESIAN_POINT ( 'NONE',  ( 2.712762565639649015, -3.052587955997662306, -3.430618716626630871 ) ) ;
#7827=ADVANCED_FACE ( 'NONE', ( #6778 ), #9515, .T. ) ;
#7865=CARTESIAN_POINT ( 'NONE',  ( 0.1750025118121568690, 4.719839900820621104, -3.469254087858248070 ) ) ;
#7877=AXIS2_PLACEMENT_3D ( 'NONE', #1152, #15798, #11856 ) ;
#7894=EDGE_CURVE ( 'NONE', #1978, #5354, #6668, .T. ) ;
#7897=ORIENTED_EDGE ( 'NONE', *, *, #10137, .F. ) ;
#7898=CARTESIAN_POINT ( 'NONE',  ( 3.999999999999999112, 2.309401076758497595, -3.504271511726784194 ) ) ;
#7900=DIRECTION ( 'NONE',  ( 0.000000000000000000, 0.000000000000000000, 1.000000000000000000 ) ) ;
#7915=CARTESIAN_POINT ( 'NONE',  ( -0.6666666666666651864, 4.233901974057260098, -3.300726591567081147 ) ) ;
#7920=CARTESIAN_POINT ( 'NONE',  ( 4.211140560182196957, -2.431303136016555122, -3.745885042887436622 ) ) ;
#7955=CARTESIAN_POINT ( 'NONE',  ( 3.333333333333332593, 2.694301256218250007, -3.300726591567078483 ) ) ;
#7987=AXIS2_PLACEMENT_3D ( 'NONE', #1557, #14405, #3360 ) ;
#7989=VERTEX_POINT ( 'NONE', #1723 ) ;
#7990=CARTESIAN_POINT ( 'NONE',  ( -4.236525694536558362, 2.416953475386465211, -3.751298745799836354 ) ) ;
#7999=CARTESIAN_POINT ( 'NONE',  ( 4.141042297810615835, -2.227970268150433863, -3.687027686973623819 ) ) ;
#8017=ORIENTED_EDGE ( 'NONE', *, *, #20957, .F. ) ;
#8026=EDGE_LOOP ( 'NONE', ( #6722, #17240, #13098 ) ) ;
#8028=EDGE_LOOP ( 'NONE', ( #21876, #344, #21715, #17173, #249 ) ) ;
#8036=EDGE_LOOP ( 'NONE', ( #20089, #23294, #13816, #7897 ) ) ;
#8049=AXIS2_PLACEMENT_3D ( 'NONE', #19004, #19243, #8140 ) ;
#8066=AXIS2_PLACEMENT_3D ( 'NONE', #12624, #7092, #18096 ) ;
#8082=EDGE_CURVE ( 'NONE', #18634, #19718, #13338, .T. ) ;
#8088=EDGE_LOOP ( 'NONE', ( #11939, #14157, #18703, #4083 ) ) ;
#8094=VERTEX_POINT ( 'NONE', #15524 ) ;
#8127=CARTESIAN_POINT ( 'NONE',  ( 0.5469614295415388128, -4.303013824935362663, -3.535263753543555598 ) ) ;
#8140=DIRECTION ( 'NONE',  ( -1.000000000000000000, 0.000000000000000000, 0.000000000000000000 ) ) ;
#8143=ORIENTED_EDGE ( 'NONE', *, *, #21164, .F. ) ;
#8159=EDGE_LOOP ( 'NONE', ( #21858, #14543, #9266, #17145 ) ) ;
#8161=CARTESIAN_POINT ( 'NONE',  ( -4.211140560182196957, -2.431303136016552013, -3.745885042887436178 ) ) ;
#8176=FACE_OUTER_BOUND ( 'NONE', #22663, .T. ) ;
#8214=CARTESIAN_POINT ( 'NONE',  ( -4.154094228333736538, -2.398367420967545627, -3.721909803043222276 ) ) ;
#8223=( NAMED_UNIT ( * ) PLANE_ANGLE_UNIT ( ) SI_UNIT ( $, .RADIAN. ) );
#8234=ORIENTED_EDGE ( 'NONE', *, *, #20443, .F. ) ;
#8239=CARTESIAN_POINT ( 'NONE',  ( 1.257172072275274388, -3.892973519170983110, -3.433252694550781303 ) ) ;
#8295=CARTESIAN_POINT ( 'NONE',  ( 5.560781378645575757, 0.000000000000000000, -4.000000000000000000 ) ) ;
#8317=VERTEX_POINT ( 'NONE', #22790 ) ;
#8326=CARTESIAN_POINT ( 'NONE',  ( -4.211140560182196957, -2.431303136016552013, -3.745885042887436178 ) ) ;
#8351=DIRECTION ( 'NONE',  ( 0.000000000000000000, 0.000000000000000000, -1.000000000000000000 ) ) ;
#8353=CARTESIAN_POINT ( 'NONE',  ( 1.274258131564866448, 3.883108878240963513, -3.220599429844046568 ) ) ;
#8375=CARTESIAN_POINT ( 'NONE',  ( 0.000000000000000000, 0.000000000000000000, 0.000000000000000000 ) ) ;
#8404=VERTEX_POINT ( 'NONE', #5304 ) ;
#8453=ORIENTED_EDGE ( 'NONE', *, *, #2171, .F. ) ;
#8477=EDGE_LOOP ( 'NONE', ( #1985, #408, #11663 ) ) ;
#8514=ORIENTED_EDGE ( 'NONE', *, *, #4824, .T. ) ;
#8525=CARTESIAN_POINT ( 'NONE',  ( 1.734723475976807094E-15, 4.618802153517012954, -0.4999999999999995559 ) ) ;
#8532=CARTESIAN_POINT ( 'NONE',  ( -4.101948962585906244, 2.368261337751074169, -3.681124513963621503 ) ) ;
#8541=DIRECTION ( 'NONE',  ( 1.000000000000000000, 0.000000000000000000, 0.000000000000000000 ) ) ;
#8576=LINE ( 'NONE', #14325, #2929 ) ;
#8609=DIRECTION ( 'NONE',  ( -1.000000000000000000, 0.000000000000000000, 0.000000000000000000 ) ) ;
#8639=CARTESIAN_POINT ( 'NONE',  ( 2.855764796983346177, -2.970025579236428737, -0.09382832055446485575 ) ) ;
#8665=VERTEX_POINT ( 'NONE', #16359 ) ;
#8704=EDGE_LOOP ( 'NONE', ( #3833, #18767, #13002, #23674 ) ) ;
#8759=CARTESIAN_POINT ( 'NONE',  ( -4.154094228333456762, 2.398367420968013253, -3.721909803043220055 ) ) ;
#8795=DIRECTION ( 'NONE',  ( 1.000000000000000000, 0.000000000000000000, 0.000000000000000000 ) ) ;
#8822=CARTESIAN_POINT ( 'NONE',  ( -2.742827927723112236, -3.035229711105190464, -3.433252694550595230 ) ) ;
#8836=CARTESIAN_POINT ( 'NONE',  ( 3.540020015735602765, 2.810662092924382627, -3.602146406945867962 ) ) ;
#8838=EDGE_CURVE ( 'NONE', #5980, #12663, #1406, .T. ) ;
#8840=CARTESIAN_POINT ( 'NONE',  ( 4.000000000000000000, 0.9868501483902631932, -0.09357334158579604100 ) ) ;
#8889=VERTEX_POINT ( 'NONE', #1082 ) ;
#8905=CARTESIAN_POINT ( 'NONE',  ( 4.211140560182196957, 2.431303136016536470, -3.745885042887433514 ) ) ;
#8906=B_SPLINE_CURVE_WITH_KNOTS ( 'NONE', 3,
 ( #8326, #8214, #18969, #9772, #11468, #15415 ),
 .UNSPECIFIED., .F., .F.,
 ( 4, 2, 4 ),
 ( -3.640115492409406142E-06, 0.0002066546034006526487, 0.0004169493222937146744 ),
 .UNSPECIFIED. ) ;
#8938=CARTESIAN_POINT ( 'NONE',  ( -4.000000000000000000, -1.560351142792950618, -0.2242961665059814425 ) ) ;
#9001=DIRECTION ( 'NONE',  ( 1.000000000000000000, 0.000000000000000000, 0.000000000000000000 ) ) ;
#9043=AXIS2_PLACEMENT_3D ( 'NONE', #8375, #21144, #11626 ) ;
#9070=CARTESIAN_POINT ( 'NONE',  ( 4.000000000000000000, 2.309401076758515803, -0.4999999999999995559 ) ) ;
#9074=FACE_OUTER_BOUND ( 'NONE', #19422, .T. ) ;
#9106=( BOUNDED_SURFACE ( )  B_SPLINE_SURFACE ( 3, 2, ( 
 ( #20203, #208, #5610 ),
 ( #16630, #1999, #457 ),
 ( #13292, #7539, #11024 ),
 ( #1771, #11147, #21883 ),
 ( #18421, #19844, #14858 ),
 ( #5491, #7428, #1890 ) ),
 .UNSPECIFIED., .F., .F., .F. ) 
 B_SPLINE_SURFACE_WITH_KNOTS ( ( 4, 2, 4 ),
 ( 3, 3 ),
 ( 0.02027065861071770947, 0.02273072267836921331, 0.02519078674602071716 ),
 ( 0.000000000000000000, 1.000000000000000000 ),
 .UNSPECIFIED. ) 
 GEOMETRIC_REPRESENTATION_ITEM ( )  RATIONAL_B_SPLINE_SURFACE ( (
 ( 1.000000000000000000, 0.8047781708337304885, 1.000000000000000000),
 ( 1.000000000000000000, 0.8123765190705307671, 1.000000000000000000),
 ( 1.000000000000000000, 0.8190656277163975707, 1.000000000000000000),
 ( 1.000000000000000000, 0.8192366903512159348, 1.000000000000000000),
 ( 1.000000000000000000, 0.8126138454302893610, 1.000000000000000000),
 ( 1.000000000000000000, 0.8047712246031417660, 1.000000000000000000) ) ) 
 REPRESENTATION_ITEM ( '' )  SURFACE ( )  );
#9184=CARTESIAN_POINT ( 'NONE',  ( -2.500000000000000444, 3.061616997868383634E-16, -25.03750572909317285 ) ) ;
#9199=VECTOR ( 'NONE', #1007, 1000.000000000000000 ) ;
#9227=CARTESIAN_POINT ( 'NONE',  ( -3.511755186886750479, 2.826662030176366081, -3.597382984111578086 ) ) ;
#9245=CARTESIAN_POINT ( 'NONE',  ( 4.000000000000000888, 1.539600717838996990, -3.300726591567079815 ) ) ;
#9266=ORIENTED_EDGE ( 'NONE', *, *, #8838, .T. ) ;
#9281=CARTESIAN_POINT ( 'NONE',  ( -4.211140560182196957, -2.431303136016552013, -3.745885042887436178 ) ) ;
#9283=CARTESIAN_POINT ( 'NONE',  ( 0.000000000000000000, 0.000000000000000000, -4.484454397937119197 ) ) ;
#9313=VERTEX_POINT ( 'NONE', #15004 ) ;
#9345=CARTESIAN_POINT ( 'NONE',  ( -4.000000000000000000, 0.8576368993457507139, -3.433240632782198709 ) ) ;
#9346=CARTESIAN_POINT ( 'NONE',  ( 0.000000000000000000, 0.000000000000000000, -5.000000000000000000 ) ) ;
#9353=CARTESIAN_POINT ( 'NONE',  ( 3.679171394226031122, 2.494631558665830973, -0.3503314178412474389 ) ) ;
#9371=FACE_OUTER_BOUND ( 'NONE', #4461, .T. ) ;
#9456=DIRECTION ( 'NONE',  ( -1.000000000000000000, 0.000000000000000000, 0.000000000000000000 ) ) ;
#9464=CARTESIAN_POINT ( 'NONE',  ( 4.211140560182196957, 2.431303136016536470, -3.745885042887433514 ) ) ;
#9466=ORIENTED_EDGE ( 'NONE', *, *, #12877, .T. ) ;
#9468=ORIENTED_EDGE ( 'NONE', *, *, #22539, .F. ) ;
#9469=LINE ( 'NONE', #16767, #10289 ) ;
#9487=CARTESIAN_POINT ( 'NONE',  ( -2.000000000000006661, 3.464101615137750834, 0.000000000000000000 ) ) ;
#9492=ORIENTED_EDGE ( 'NONE', *, *, #14521, .T. ) ;
#9515=CONICAL_SURFACE ( 'NONE', #5663, 5.560781378645573980, 1.221730476396046816 ) ;
#9521=CARTESIAN_POINT ( 'NONE',  ( 2.000000000000000444, 3.464101615137754830, -3.142992957459231018 ) ) ;
#9557=CARTESIAN_POINT ( 'NONE',  ( 0.3208286057739604957, -4.433571671609698228, -0.3503314178412692548 ) ) ;
#9567=CARTESIAN_POINT ( 'NONE',  ( 0.6640947660595348800, -4.471078309994175548, -3.602146406945708090 ) ) ;
#9591=CONICAL_SURFACE ( 'NONE', #3818, 2.059999999999998721, 0.9599310885968738161 ) ;
#9662=CARTESIAN_POINT ( 'NONE',  ( 1.567478505476134606E-15, 4.618802153517012066, -5.000000000000000000 ) ) ;
#9674=CARTESIAN_POINT ( 'NONE',  ( 0.02448733951239481094, 4.877042772274728044, -3.751161874094022242 ) ) ;
#9682=FACE_OUTER_BOUND ( 'NONE', #18633, .T. ) ;
#9700=CARTESIAN_POINT ( 'NONE',  ( -4.000000000000000000, 0.8730739991738342143, -3.223134629628428893 ) ) ;
#9719=CIRCLE ( 'NONE', #22305, 2.499999999999999556 ) ;
#9741=ORIENTED_EDGE ( 'NONE', *, *, #5989, .F. ) ;
#9760=PRODUCT_DEFINITION ( 'UNKNOWN', '', #4180, #439 ) ;
#9767=CARTESIAN_POINT ( 'NONE',  ( 0.000000000000000000, 0.000000000000000000, -5.000000000000000888 ) ) ;
#9771=DIRECTION ( 'NONE',  ( -0.9396926207859138680, 0.000000000000000000, -0.3420201433256536139 ) ) ;
#9772=CARTESIAN_POINT ( 'NONE',  ( -4.024497503033519941, -2.323544716729390558, -3.572167766733381544 ) ) ;
#9800=CIRCLE ( 'NONE', #17060, 2.500000000000000888 ) ;
#9805=CONICAL_SURFACE ( 'NONE', #9043, 4.000000000000000000, 0.8911886515913786111 ) ;
#9812=ORIENTED_EDGE ( 'NONE', *, *, #19903, .F. ) ;
#9819=CARTESIAN_POINT ( 'NONE',  ( 4.000000000000000000, 2.309401076758497151, -3.433295621305379353 ) ) ;
#9841=FACE_OUTER_BOUND ( 'NONE', #1666, .T. ) ;
#9919=CARTESIAN_POINT ( 'NONE',  ( -2.000000000000007550, -3.464101615137749945, 0.000000000000000000 ) ) ;
#9991=AXIS2_PLACEMENT_3D ( 'NONE', #4800, #14036, #17636 ) ;
#10002=CARTESIAN_POINT ( 'NONE',  ( -2.500000000000000888, 0.000000000000000000, -4.974599999999998801 ) ) ;
#10040=ORIENTED_EDGE ( 'NONE', *, *, #15851, .F. ) ;
#10048=CARTESIAN_POINT ( 'NONE',  ( -0.1404048886732797152, -4.699864953788083888, -3.686887068327043160 ) ) ;
#10074=EDGE_CURVE ( 'NONE', #10654, #17879, #17619, .T. ) ;
#10137=EDGE_CURVE ( 'NONE', #1712, #5354, #7291, .T. ) ;
#10148=LINE ( 'NONE', #19102, #9199 ) ;
#10150=FACE_OUTER_BOUND ( 'NONE', #8477, .T. ) ;
#10185=CARTESIAN_POINT ( 'NONE',  ( -4.000000000000000000, -2.309401076758512694, -5.000000000000000000 ) ) ;
#10197=CARTESIAN_POINT ( 'NONE',  ( -3.333333333333332149, -2.694301256218264218, -3.300726591567082036 ) ) ;
#10217=ORIENTED_EDGE ( 'NONE', *, *, #904, .T. ) ;
#10237=APPLICATION_CONTEXT ( 'automotive_design' ) ;
#10262=CARTESIAN_POINT ( 'NONE',  ( -4.198928548860774157, 0.8158838809860065044, -3.526471437616918170 ) ) ;
#10289=VECTOR ( 'NONE', #13191, 999.9999999999998863 ) ;
#10293=B_SPLINE_CURVE_WITH_KNOTS ( 'NONE', 3,
 ( #22925, #21109, #10262, #4725, #16195, #17318 ),
 .UNSPECIFIED., .F., .F.,
 ( 4, 2, 4 ),
 ( 0.002452478801916376308, 0.003676905084148007850, 0.004901331366379639391 ),
 .UNSPECIFIED. ) ;
#10309=CARTESIAN_POINT ( 'NONE',  ( 0.000000000000000000, 0.000000000000000000, -4.974599999999998801 ) ) ;
#10318=CARTESIAN_POINT ( 'NONE',  ( -3.680118525130244400, 2.494084732383327285, -0.3507732604232449702 ) ) ;
#10320=VERTEX_POINT ( 'NONE', #15953 ) ;
#10334=ADVANCED_FACE ( 'NONE', ( #4928, #21671 ), #10822, .F. ) ;
#10353=DIRECTION ( 'NONE',  ( -0.000000000000000000, -0.000000000000000000, 1.000000000000000000 ) ) ;
#10396=CARTESIAN_POINT ( 'NONE',  ( -4.235886605889389145, -2.417314728048544303, -3.751161874094020909 ) ) ;
#10429=FACE_OUTER_BOUND ( 'NONE', #818, .T. ) ;
#10432=ORIENTED_EDGE ( 'NONE', *, *, #15851, .T. ) ;
#10434=EDGE_CURVE ( 'NONE', #12663, #16821, #22904, .T. ) ;
#10465=EDGE_CURVE ( 'NONE', #7262, #20390, #5597, .T. ) ;
#10469=CARTESIAN_POINT ( 'NONE',  ( -3.349226789952655547, -2.685125164760744809, -0.2236248678334863682 ) ) ;
#10485=CONICAL_SURFACE ( 'NONE', #3558, 4.000000000000000000, 0.8911886515913786111 ) ;
#10515=AXIS2_PLACEMENT_3D ( 'NONE', #12120, #6598, #2978 ) ;
#10519=CARTESIAN_POINT ( 'NONE',  ( -0.1410422978106123659, 4.700232962125094893, -3.687027686973624707 ) ) ;
#10522=VECTOR ( 'NONE', #17406, 1000.000000000000114 ) ;
#10524=B_SPLINE_CURVE_WITH_KNOTS ( 'NONE', 3,
 ( #11758, #10197, #19260, #3094, #22980 ),
 .UNSPECIFIED., .F., .F.,
 ( 4, 1, 4 ),
 ( 0.000000000000000000, 0.002309401076758505356, 0.004618802153517010713 ),
 .UNSPECIFIED. ) ;
#10589=CARTESIAN_POINT ( 'NONE',  ( -2.804994570502171047, -3.229033611042465335, -3.526374918436838701 ) ) ;
#10606=LINE ( 'NONE', #21686, #20858 ) ;
#10627=CARTESIAN_POINT ( 'NONE',  ( -3.453038570459499024, -2.625189405340453419, -3.535263753545272891 ) ) ;
#10633=ORIENTED_EDGE ( 'NONE', *, *, #7894, .F. ) ;
#10636=DIRECTION ( 'NONE',  ( -1.000000000000000000, 0.000000000000000000, 0.000000000000000000 ) ) ;
#10641=CARTESIAN_POINT ( 'NONE',  ( 4.000000000000000000, 0.3987449864460005378, -0.01220643443059817035 ) ) ;
#10654=VERTEX_POINT ( 'NONE', #8161 ) ;
#10655=CARTESIAN_POINT ( 'NONE',  ( 0.000000000000000000, 0.000000000000000000, -0.3080913168122742518 ) ) ;
#10671=DIRECTION ( 'NONE',  ( 0.000000000000000000, 0.000000000000000000, 1.000000000000000000 ) ) ;
#10674=CARTESIAN_POINT ( 'NONE',  ( 1.411581201560190495E-15, 4.862606272033091592, -3.745885042887436622 ) ) ;
#10682=ORIENTED_EDGE ( 'NONE', *, *, #4335, .F. ) ;
#10686=DIRECTION ( 'NONE',  ( 0.000000000000000000, 0.000000000000000000, 1.000000000000000000 ) ) ;
#10745=DIRECTION ( 'NONE',  ( 0.000000000000000000, 0.000000000000000000, 1.000000000000000000 ) ) ;
#10775=CARTESIAN_POINT ( 'NONE',  ( 0.000000000000000000, 0.000000000000000000, -4.974599999999998801 ) ) ;
#10813=CARTESIAN_POINT ( 'NONE',  ( -6.259644161404860030E-16, -4.618802153517027165, -5.000000000000000000 ) ) ;
#10822=PLANE ( 'NONE',  #8066 ) ;
#10856=FACE_OUTER_BOUND ( 'NONE', #8088, .T. ) ;
#10882=DIRECTION ( 'NONE',  ( 1.000000000000000000, 0.000000000000000000, 0.000000000000000000 ) ) ;
#10900=CARTESIAN_POINT ( 'NONE',  ( -4.000000000000000000, 2.309401076758498483, -5.000000000000000000 ) ) ;
#10936=CARTESIAN_POINT ( 'NONE',  ( -6.259644161404862988E-16, -4.618802153517027165, -3.504271511726793076 ) ) ;
#11000=CARTESIAN_POINT ( 'NONE',  ( 2.500000000000000888, 3.061616997868384127E-16, -4.974599999999998801 ) ) ;
#11024=CARTESIAN_POINT ( 'NONE',  ( 4.197478902586992966, -0.8524102783748346290, -3.505063281295504041 ) ) ;
#11026=PLANE ( 'NONE',  #2412 ) ;
#11040=LINE ( 'NONE', #1553, #797 ) ;
#11096=DIRECTION ( 'NONE',  ( 0.000000000000000000, 0.000000000000000000, 1.000000000000000000 ) ) ;
#11118=CARTESIAN_POINT ( 'NONE',  ( 0.6507732100473444525, -4.243078065514795050, -0.2236248678334952777 ) ) ;
#11144=CARTESIAN_POINT ( 'NONE',  ( 0.000000000000000000, 0.000000000000000000, -0.3080913168122742518 ) ) ;
#11147=CARTESIAN_POINT ( 'NONE',  ( 4.000000000000000888, 0.8228435280416209752, -3.430609588141487976 ) ) ;
#11150=CARTESIAN_POINT ( 'NONE',  ( -4.204114297095464359, 1.660363174096617156, -3.602136431857887011 ) ) ;
#11152=FACE_OUTER_BOUND ( 'NONE', #3611, .T. ) ;
#11155=CARTESIAN_POINT ( 'NONE',  ( -3.999999999999999112, 1.539600717838996324, -3.300726591567078039 ) ) ;
#11177=CARTESIAN_POINT ( 'NONE',  ( -5.560781378645575757, 6.809993116116508640E-16, -4.000000000000000000 ) ) ;
#11211=AXIS2_PLACEMENT_3D ( 'NONE', #22242, #18426, #2003 ) ;
#11213=ORIENTED_EDGE ( 'NONE', *, *, #16815, .F. ) ;
#11231=ORIENTED_EDGE ( 'NONE', *, *, #12812, .T. ) ;
#11257=DIRECTION ( 'NONE',  ( -0.8191520442889875797, 1.003171929053519570E-16, 0.5735764363510522656 ) ) ;
#11271=CARTESIAN_POINT ( 'NONE',  ( 2.344047193898588954, 3.265465875126468021, -5.031375706690542042E-16 ) ) ;
#11276=CARTESIAN_POINT ( 'NONE',  ( 0.000000000000000000, 0.000000000000000000, -0.2800830152838844622 ) ) ;
#11317=ADVANCED_FACE ( 'NONE', ( #9371 ), #16783, .F. ) ;
#11348=CARTESIAN_POINT ( 'NONE',  ( -0.6507732100473471171, 4.243078065514775510, -0.2236248678334823436 ) ) ;
#11355=EDGE_LOOP ( 'NONE', ( #18075, #20886, #18795, #5330, #5773, #6251 ) ) ;
#11379=ORIENTED_EDGE ( 'NONE', *, *, #19748, .F. ) ;
#11398=CIRCLE ( 'NONE', #4104, 4.000000000000000000 ) ;
#11410=B_SPLINE_CURVE_WITH_KNOTS ( 'NONE', 3,
 ( #1424, #5042, #12373, #7084, #2, #7333, #19637, #3356 ),
 .UNSPECIFIED., .F., .F.,
 ( 4, 2, 2, 4 ),
 ( 0.005725059856848641743, 0.006314084072593626612, 0.006903108288338611481, 0.008081156719828581220 ),
 .UNSPECIFIED. ) ;
#11442=DIRECTION ( 'NONE',  ( -0.8660254037844373753, 0.5000000000000021094, 0.000000000000000000 ) ) ;
#11448=CARTESIAN_POINT ( 'NONE',  ( 4.000000000000000000, 2.309401076758497151, -3.433295621305379353 ) ) ;
#11468=CARTESIAN_POINT ( 'NONE',  ( -4.000000000000000888, -2.309401076758512694, -3.504269196027526512 ) ) ;
#11482=CARTESIAN_POINT ( 'NONE',  ( 0.1404048886732821022, 4.699864953788070565, -3.686887068327037387 ) ) ;
#11489=B_SPLINE_CURVE_WITH_KNOTS ( 'NONE', 3,
 ( #3691, #11155, #14865, #2007, #5500 ),
 .UNSPECIFIED., .F., .F.,
 ( 4, 1, 4 ),
 ( 0.000000000000000000, 0.002309401076758505790, 0.004618802153517011580 ),
 .UNSPECIFIED. ) ;
#11522=AXIS2_PLACEMENT_3D ( 'NONE', #2283, #13327, #12855 ) ;
#11585=B_SPLINE_CURVE_WITH_KNOTS ( 'NONE', 3,
 ( #12502, #21547, #12261, #23600, #10589, #21429, #21304, #15951 ),
 .UNSPECIFIED., .F., .F.,
 ( 4, 2, 2, 4 ),
 ( 0.000000000000000000, 0.002450665683189818828, 0.003675998524784728459, 0.004901331366379638524 ),
 .UNSPECIFIED. ) ;
#11599=ORIENTED_EDGE ( 'NONE', *, *, #12687, .F. ) ;
#11600=CARTESIAN_POINT ( 'NONE',  ( -4.175648173966055587, 2.207990556236529844, -3.469390959564062626 ) ) ;
#11614=ORIENTED_EDGE ( 'NONE', *, *, #3689, .F. ) ;
#11626=DIRECTION ( 'NONE',  ( -1.000000000000000000, 0.000000000000000000, 0.000000000000000000 ) ) ;
#11663=ORIENTED_EDGE ( 'NONE', *, *, #21029, .F. ) ;
#11712=DIRECTION ( 'NONE',  ( 0.000000000000000000, 0.000000000000000000, -1.000000000000000000 ) ) ;
#11715=CARTESIAN_POINT ( 'NONE',  ( -1.243802165048909503, 3.900692638707381921, -3.223146290109805800 ) ) ;
#11723=CARTESIAN_POINT ( 'NONE',  ( 0.5276280594147412240, -4.314175951381924889, -3.320322319201654881 ) ) ;
#11758=CARTESIAN_POINT ( 'NONE',  ( -4.000000000000000000, -2.309401076758512694, -3.433295621305382461 ) ) ;
#11762=ADVANCED_FACE ( 'NONE', ( #3812 ), #9106, .F. ) ;
#11793=DIRECTION ( 'NONE',  ( 0.000000000000000000, 0.000000000000000000, -1.000000000000000000 ) ) ;
#11818=COLOUR_RGB ( '', 0.40784314, 0.44705882, 0.49803922) ;
#11836=EDGE_LOOP ( 'NONE', ( #19312, #12581, #446, #16519 ) ) ;
#11856=DIRECTION ( 'NONE',  ( 1.000000000000000000, 0.000000000000000000, 0.000000000000000000 ) ) ;
#11865=CARTESIAN_POINT ( 'NONE',  ( 4.024499207728657879, 2.323545700935571556, -3.572172305156506411 ) ) ;
#11870=ORIENTED_EDGE ( 'NONE', *, *, #17587, .F. ) ;
#11901=ADVANCED_FACE ( 'NONE', ( #4643, #15451 ), #2596, .T. ) ;
#11909=CIRCLE ( 'NONE', #9991, 5.384454397937118664 ) ;
#11939=ORIENTED_EDGE ( 'NONE', *, *, #14986, .F. ) ;
#11953=CARTESIAN_POINT ( 'NONE',  ( 4.101954839143059139, -2.368264730582948285, -3.681130640444269631 ) ) ;
#11954=FACE_OUTER_BOUND ( 'NONE', #4709, .T. ) ;
#11964=CARTESIAN_POINT ( 'NONE',  ( 3.472371940585993855, 2.614027278893175321, -3.320322319201766792 ) ) ;
#11981=CARTESIAN_POINT ( 'NONE',  ( 1.747541505913279281, -3.837784562140273081, -3.503702292528912299 ) ) ;
#12036=ORIENTED_EDGE ( 'NONE', *, *, #18486, .T. ) ;
#12092=DIRECTION ( 'NONE',  ( -0.000000000000000000, -0.000000000000000000, 1.000000000000000000 ) ) ;
#12093=CARTESIAN_POINT ( 'NONE',  ( 0.000000000000000000, 0.000000000000000000, 3.469446951953614189E-15 ) ) ;
#12096=CARTESIAN_POINT ( 'NONE',  ( 2.805705207896068476, -3.226868319750173075, -3.503898532754370354 ) ) ;
#12098=AXIS2_PLACEMENT_3D ( 'NONE', #17389, #19051, #19173 ) ;
#12107=CIRCLE ( 'NONE', #971, 2.499999999999999556 ) ;
#12111=EDGE_LOOP ( 'NONE', ( #16267, #22096, #19135, #21884, #17508, #21330, #21238 ) ) ;
#12120=CARTESIAN_POINT ( 'NONE',  ( 0.000000000000000000, 0.000000000000000000, -4.694516984716113228 ) ) ;
#12131=ORIENTED_EDGE ( 'NONE', *, *, #12812, .F. ) ;
#12152=ADVANCED_FACE ( 'NONE', ( #4756 ), #9591, .F. ) ;
#12180=DIRECTION ( 'NONE',  ( 1.000000000000000000, 0.000000000000000000, 0.000000000000000000 ) ) ;
#12191=DIRECTION ( 'NONE',  ( 0.000000000000000000, 0.000000000000000000, 1.000000000000000000 ) ) ;
#12261=CARTESIAN_POINT ( 'NONE',  ( -1.391697335622809950, -4.043246145443391448, -3.503898532754372575 ) ) ;
#12275=ORIENTED_EDGE ( 'NONE', *, *, #10434, .T. ) ;
#12278=( NAMED_UNIT ( * ) SI_UNIT ( $, .STERADIAN. ) SOLID_ANGLE_UNIT ( ) );
#12289=CARTESIAN_POINT ( 'NONE',  ( 0.000000000000000000, 0.000000000000000000, -5.000000000000000000 ) ) ;
#12342=ORIENTED_EDGE ( 'NONE', *, *, #5227, .F. ) ;
#12373=CARTESIAN_POINT ( 'NONE',  ( -4.000000000000000000, 0.3987449864459974846, -0.01220643443059782861 ) ) ;
#12447=EDGE_CURVE ( 'NONE', #14331, #16324, #22225, .T. ) ;
#12456=CIRCLE ( 'NONE', #14743, 4.000000000000000000 ) ;
#12479=ADVANCED_FACE ( 'NONE', ( #13268 ), #15555, .F. ) ;
#12484=DIRECTION ( 'NONE',  ( -1.000000000000000000, 0.000000000000000000, 0.000000000000000000 ) ) ;
#12502=CARTESIAN_POINT ( 'NONE',  ( -6.473970235329672780E-16, -4.862606272033106691, -3.745885042887442395 ) ) ;
#12513=EDGE_LOOP ( 'NONE', ( #14814, #5588, #12548, #17204 ) ) ;
#12539=CARTESIAN_POINT ( 'NONE',  ( -4.000000000000000000, -0.3979232138631226823, -3.896351557369779711E-17 ) ) ;
#12548=ORIENTED_EDGE ( 'NONE', *, *, #5227, .T. ) ;
#12581=ORIENTED_EDGE ( 'NONE', *, *, #3662, .F. ) ;
#12593=CARTESIAN_POINT ( 'NONE',  ( -0.6937372685066653943, 4.453844082567723461, -3.610536846335889116 ) ) ;
#12605=ORIENTED_EDGE ( 'NONE', *, *, #1261, .T. ) ;
#12624=CARTESIAN_POINT ( 'NONE',  ( 8.673617379884035472E-16, 4.618802153517012954, 0.000000000000000000 ) ) ;
#12663=VERTEX_POINT ( 'NONE', #8295 ) ;
#12687=EDGE_CURVE ( 'NONE', #5642, #5980, #11909, .T. ) ;
#12691=B_SPLINE_CURVE_WITH_KNOTS ( 'NONE', 3,
 ( #15540, #17441, #17556, #15656, #22928 ),
 .UNSPECIFIED., .F., .F.,
 ( 4, 1, 4 ),
 ( 5.640274452250024914E-20, 0.002309401076758505356, 0.004618802153517010713 ),
 .UNSPECIFIED. ) ;
#12750=ORIENTED_EDGE ( 'NONE', *, *, #12447, .F. ) ;
#12812=EDGE_CURVE ( 'NONE', #10320, #19958, #11410, .T. ) ;
#12823=DIRECTION ( 'NONE',  ( 1.000000000000000000, 0.000000000000000000, 0.000000000000000000 ) ) ;
#12850=CARTESIAN_POINT ( 'NONE',  ( 4.198928548860774157, -0.8158838809860124996, -3.526471437616918170 ) ) ;
#12855=DIRECTION ( 'NONE',  ( -1.000000000000000000, 0.000000000000000000, 0.000000000000000000 ) ) ;
#12877=EDGE_CURVE ( 'NONE', #9313, #12663, #11040, .T. ) ;
#12879=ADVANCED_FACE ( 'NONE', ( #21665 ), #1672, .T. ) ;
#12922=CONICAL_SURFACE ( 'NONE', #15971, 5.560781378645573980, 1.221730476396046816 ) ;
#12953=CARTESIAN_POINT ( 'NONE',  ( 4.000000000000000000, -2.309401076758514915, -3.433295621305383349 ) ) ;
#13002=ORIENTED_EDGE ( 'NONE', *, *, #20443, .T. ) ;
#13026=DIRECTION ( 'NONE',  ( -0.5000000000000016653, 0.8660254037844378194, 0.000000000000000000 ) ) ;
#13048=EDGE_CURVE ( 'NONE', #5354, #1712, #22179, .T. ) ;
#13072=CARTESIAN_POINT ( 'NONE',  ( 1.312671235360372224, 3.860931062424219462, -0.05923475698270440348 ) ) ;
#13098=ORIENTED_EDGE ( 'NONE', *, *, #5499, .F. ) ;
#13139=CARTESIAN_POINT ( 'NONE',  ( -0.3208286057739654917, 4.433571671609680465, -0.3503314178412548774 ) ) ;
#13176=CARTESIAN_POINT ( 'NONE',  ( 2.499999999999999556, 0.000000000000000000, 3.469446951953614189E-15 ) ) ;
#13191=DIRECTION ( 'NONE',  ( 0.8191520442889875797, 0.000000000000000000, 0.5735764363510522656 ) ) ;
#13197=CARTESIAN_POINT ( 'NONE',  ( -4.000000000000000000, 2.309401076758498483, -5.000000000000000000 ) ) ;
#13235=LINE ( 'NONE', #10002, #10522 ) ;
#13242=VECTOR ( 'NONE', #7611, 1000.000000000000000 ) ;
#13246=EDGE_CURVE ( 'NONE', #16324, #16789, #14253, .T. ) ;
#13268=FACE_OUTER_BOUND ( 'NONE', #4143, .T. ) ;
#13280=ADVANCED_FACE ( 'NONE', ( #13984 ), #1033, .T. ) ;
#13292=CARTESIAN_POINT ( 'NONE',  ( 4.000000000000000000, -0.8732470631449981147, -3.223155494240760088 ) ) ;
#13314=ORIENTED_EDGE ( 'NONE', *, *, #8082, .F. ) ;
#13327=DIRECTION ( 'NONE',  ( -0.000000000000000000, 0.000000000000000000, -1.000000000000000000 ) ) ;
#13338=CIRCLE ( 'NONE', #2969, 2.500000000000000444 ) ;
#13353=EDGE_CURVE ( 'NONE', #17879, #16821, #19316, .T. ) ;
#13363=AXIS2_PLACEMENT_3D ( 'NONE', #2880, #11793, #17046 ) ;
#13393=CARTESIAN_POINT ( 'NONE',  ( -1.360585162435467455, 4.061296242128285883, -3.505054077164959203 ) ) ;
#13403=AXIS2_PLACEMENT_3D ( 'NONE', #5217, #20523, #22438 ) ;
#13434=B_SPLINE_CURVE_WITH_KNOTS ( 'NONE', 3,
 ( #18337, #16781, #12850, #14534, #21673, #5282 ),
 .UNSPECIFIED., .F., .F.,
 ( 4, 2, 4 ),
 ( 0.002452478801916361129, 0.003676905084148001344, 0.004901331366379641126 ),
 .UNSPECIFIED. ) ;
#13507=CARTESIAN_POINT ( 'NONE',  ( 3.999999999999999112, -0.3979232138631231819, -5.929230630780099908E-17 ) ) ;
#13586=ADVANCED_FACE ( 'NONE', ( #14197 ), #6757, .F. ) ;
#13594=CARTESIAN_POINT ( 'NONE',  ( -4.000000000000000000, -2.309401076758515803, -0.4999999999999995559 ) ) ;
#13600=DIRECTION ( 'NONE',  ( 0.000000000000000000, -0.000000000000000000, 1.000000000000000000 ) ) ;
#13630=CARTESIAN_POINT ( 'NONE',  ( 4.236525694536557474, -2.416953475386482530, -3.751298745799839462 ) ) ;
#13640=EDGE_CURVE ( 'NONE', #16324, #8317, #11398, .T. ) ;
#13663=CARTESIAN_POINT ( 'NONE',  ( -2.687328764639638656, 3.067272167851286202, -0.05923475698270370959 ) ) ;
#13739=CARTESIAN_POINT ( 'NONE',  ( -2.807080416178626692, 3.225969019225154444, -3.502507215260441065 ) ) ;
#13770=DIRECTION ( 'NONE',  ( 1.000000000000000000, 0.000000000000000000, 0.000000000000000000 ) ) ;
#13776=EDGE_CURVE ( 'NONE', #16324, #20947, #7576, .T. ) ;
#13788=EDGE_CURVE ( 'NONE', #19958, #23289, #4759, .T. ) ;
#13816=ORIENTED_EDGE ( 'NONE', *, *, #7894, .T. ) ;
#13838=PRESENTATION_STYLE_ASSIGNMENT (( #15634 ) ) ;
#13845=EDGE_CURVE ( 'NONE', #21424, #21411, #10524, .T. ) ;
#13916=CARTESIAN_POINT ( 'NONE',  ( 0.000000000000000000, 0.000000000000000000, 3.469446951953614189E-15 ) ) ;
#13930=AXIS2_PLACEMENT_3D ( 'NONE', #3649, #13026, #16483 ) ;
#13984=FACE_OUTER_BOUND ( 'NONE', #17376, .T. ) ;
#14030=CARTESIAN_POINT ( 'NONE',  ( 2.000000000000005329, -3.464101615137751722, 0.000000000000000000 ) ) ;
#14036=DIRECTION ( 'NONE',  ( -0.000000000000000000, -0.000000000000000000, 1.000000000000000000 ) ) ;
#14054=FILL_AREA_STYLE_COLOUR ( '', #11818 ) ;
#14109=CIRCLE ( 'NONE', #3752, 0.5155456020628804703 ) ;
#14145=ORIENTED_EDGE ( 'NONE', *, *, #13048, .F. ) ;
#14153=DIRECTION ( 'NONE',  ( -0.000000000000000000, 0.000000000000000000, -1.000000000000000000 ) ) ;
#14157=ORIENTED_EDGE ( 'NONE', *, *, #1429, .F. ) ;
#14182=ORIENTED_EDGE ( 'NONE', *, *, #16513, .T. ) ;
#14197=FACE_OUTER_BOUND ( 'NONE', #8036, .T. ) ;
#14253=B_SPLINE_CURVE_WITH_KNOTS ( 'NONE', 3,
 ( #14343, #18147, #10641, #6909, #8840, #5214, #3423, #9070 ),
 .UNSPECIFIED., .F., .F.,
 ( 4, 2, 2, 4 ),
 ( 0.005725059856848645212, 0.006314084072593634418, 0.006903108288338624492, 0.008081156719828603771 ),
 .UNSPECIFIED. ) ;
#14278=CARTESIAN_POINT ( 'NONE',  ( -4.000000000000004441, 2.309401076758496263, -3.504269196027523847 ) ) ;
#14314=CLOSED_SHELL ( 'NONE', ( #18891, #20710, #4100, #7827, #17108, #2630, #13586, #282, #1865, #11317, #12879, #721, #14842, #10334, #11901, #1863, #5432, #13280, #20234, #14774, #852, #2762, #5155, #19054, #21694, #5006, #11762, #12479, #21852, #12152, #7475, #7277 ) ) ;
#14325=CARTESIAN_POINT ( 'NONE',  ( 2.500000000000000888, 3.061616997868384127E-16, -4.974599999999998801 ) ) ;
#14326=CARTESIAN_POINT ( 'NONE',  ( -1.287237434361707233, -3.875615274277397937, -3.430618716626816500 ) ) ;
#14331=VERTEX_POINT ( 'NONE', #23225 ) ;
#14337=ORIENTED_EDGE ( 'NONE', *, *, #13845, .T. ) ;
#14343=CARTESIAN_POINT ( 'NONE',  ( 4.000000000000000000, 0.000000000000000000, 0.000000000000000000 ) ) ;
#14405=DIRECTION ( 'NONE',  ( 0.000000000000000000, 0.000000000000000000, -1.000000000000000000 ) ) ;
#14440=DIRECTION ( 'NONE',  ( -1.000000000000000000, 0.000000000000000000, 0.000000000000000000 ) ) ;
#14457=VECTOR ( 'NONE', #9771, 1000.000000000000227 ) ;
#14496=ORIENTED_EDGE ( 'NONE', *, *, #14808, .T. ) ;
#14507=FACE_OUTER_BOUND ( 'NONE', #268, .T. ) ;
#14516=CARTESIAN_POINT ( 'NONE',  ( 2.345747346278113987, -3.264484291692503870, -0.01223254789874484924 ) ) ;
#14521=EDGE_CURVE ( 'NONE', #5354, #946, #9469, .T. ) ;
#14525=DIRECTION ( 'NONE',  ( 0.8660254037844379305, 0.5000000000000013323, 0.000000000000000000 ) ) ;
#14534=CARTESIAN_POINT ( 'NONE',  ( 4.204015924366189871, -1.626724848190933548, -3.610627190413393084 ) ) ;
#14543=ORIENTED_EDGE ( 'NONE', *, *, #12687, .T. ) ;
#14558=AXIS2_PLACEMENT_3D ( 'NONE', #16228, #16341, #14440 ) ;
#14595=CARTESIAN_POINT ( 'NONE',  ( -4.197393957002303999, -7.773935952363655451E-14, -3.503767560748929810 ) ) ;
#14617=CARTESIAN_POINT ( 'NONE',  ( -1.747541505913277282, 3.837784562140256650, -3.503702292528906526 ) ) ;
#14639=DIRECTION ( 'NONE',  ( 0.5000000000000013323, -0.8660254037844379305, 0.000000000000000000 ) ) ;
#14663=ORIENTED_EDGE ( 'NONE', *, *, #15357, .T. ) ;
#14729=CARTESIAN_POINT ( 'NONE',  ( -5.384454397937118664, 6.594054843588581554E-16, -4.484454397937119197 ) ) ;
#14740=CARTESIAN_POINT ( 'NONE',  ( -4.000000000000000000, 2.471528634177585282, -3.686887442155186712 ) ) ;
#14743=AXIS2_PLACEMENT_3D ( 'NONE', #17735, #17630, #19517 ) ;
#14748=CARTESIAN_POINT ( 'NONE',  ( 1.144235203016666258, 3.958177651039090250, -0.09382832055445661235 ) ) ;
#14750=ORIENTED_EDGE ( 'NONE', *, *, #2501, .T. ) ;
#14758=DIRECTION ( 'NONE',  ( 1.000000000000000000, 0.000000000000000000, 0.000000000000000000 ) ) ;
#14774=ADVANCED_FACE ( 'NONE', ( #19758 ), #4911, .T. ) ;
#14800=CARTESIAN_POINT ( 'NONE',  ( 1.567478505476134606E-15, 4.618802153517012066, -3.433295621305382905 ) ) ;
#14808=EDGE_CURVE ( 'NONE', #5642, #16821, #14109, .T. ) ;
#14814=ORIENTED_EDGE ( 'NONE', *, *, #13048, .T. ) ;
#14830=CARTESIAN_POINT ( 'NONE',  ( 1.655952806101427033, -3.662737355149048302, -1.182683869819604841E-14 ) ) ;
#14842=ADVANCED_FACE ( 'NONE', ( #19849 ), #3209, .T. ) ;
#14858=CARTESIAN_POINT ( 'NONE',  ( 4.203935335434060505, 1.640780671294165272, -3.598452447879202598 ) ) ;
#14861=CARTESIAN_POINT ( 'NONE',  ( -4.211405944401398038, -2.460460786169389902, -3.751298493805494072 ) ) ;
#14862=DIRECTION ( 'NONE',  ( 1.000000000000000000, 0.000000000000000000, 0.000000000000000000 ) ) ;
#14864=ORIENTED_EDGE ( 'NONE', *, *, #19748, .T. ) ;
#14865=CARTESIAN_POINT ( 'NONE',  ( -4.000000000000000000, -7.806255641895631925E-15, -3.142992957459232350 ) ) ;
#14907=AXIS2_PLACEMENT_3D ( 'NONE', #10900, #6943, #10671 ) ;
#14921=B_SPLINE_CURVE_WITH_KNOTS ( 'NONE', 3,
 ( #9819, #7898, #11865, #15103, #22723, #20803 ),
 .UNSPECIFIED., .F., .F.,
 ( 4, 2, 4 ),
 ( 0.000000000000000000, 0.0002095117440854730670, 0.0004190234881709461339 ),
 .UNSPECIFIED. ) ;
#14929=CARTESIAN_POINT ( 'NONE',  ( 0.1756481739660539498, -4.720212674038995360, -3.469390959564070620 ) ) ;
#14986=EDGE_CURVE ( 'NONE', #10654, #21424, #8906, .T. ) ;
#14997=CARTESIAN_POINT ( 'NONE',  ( 0.000000000000000000, 0.000000000000000000, -25.03750572909317285 ) ) ;
#15004=CARTESIAN_POINT ( 'NONE',  ( 4.197393957002303999, 7.772902908466098641E-14, -3.503767560748929810 ) ) ;
#15008=CARTESIAN_POINT ( 'NONE',  ( 0.000000000000000000, 0.000000000000000000, -5.000000000000000888 ) ) ;
#15024=VERTEX_POINT ( 'NONE', #17070 ) ;
#15045=( LENGTH_UNIT ( ) NAMED_UNIT ( * ) SI_UNIT ( .MILLI., .METRE. ) );
#15048=CONICAL_SURFACE ( 'NONE', #11211, 4.000000000000000000, 0.8911886515913786111 ) ;
#15050=DIRECTION ( 'NONE',  ( -0.000000000000000000, -0.000000000000000000, 1.000000000000000000 ) ) ;
#15053=EDGE_CURVE ( 'NONE', #15024, #23683, #18853, .T. ) ;
#15103=CARTESIAN_POINT ( 'NONE',  ( 4.101954839143060028, 2.368264730582927857, -3.681130640444267854 ) ) ;
#15119=LINE ( 'NONE', #13197, #20226 ) ;
#15123=CARTESIAN_POINT ( 'NONE',  ( 0.000000000000000000, 0.000000000000000000, -4.484454397937119197 ) ) ;
#15125=CARTESIAN_POINT ( 'NONE',  ( 4.000000000000000000, 2.309401076758497151, -5.000000000000000000 ) ) ;
#15138=ORIENTED_EDGE ( 'NONE', *, *, #3835, .T. ) ;
#15152=DIRECTION ( 'NONE',  ( 1.000000000000000000, 0.000000000000000000, 0.000000000000000000 ) ) ;
#15187=CARTESIAN_POINT ( 'NONE',  ( -0.5469614295416921346, 4.303013824936271270, -3.535263753543735454 ) ) ;
#15212=FACE_OUTER_BOUND ( 'NONE', #6857, .T. ) ;
#15254=ORIENTED_EDGE ( 'NONE', *, *, #10137, .T. ) ;
#15262=AXIS2_PLACEMENT_3D ( 'NONE', #9283, #38, #15152 ) ;
#15290=PRODUCT ( 'hex flange nut gradea_iso_ISO - 4161 - M5 - N', 'hex flange nut gradea_iso_ISO - 4161 - M5 - N', '', ( #2405 ) ) ;
#15311=CARTESIAN_POINT ( 'NONE',  ( -0.6640947660597427138, 4.471078309994878985, -3.602146406945963442 ) ) ;
#15317=ORIENTED_EDGE ( 'NONE', *, *, #22829, .T. ) ;
#15326=CIRCLE ( 'NONE', #16453, 2.500000000000000888 ) ;
#15349=ORIENTED_EDGE ( 'NONE', *, *, #3689, .T. ) ;
#15357=EDGE_CURVE ( 'NONE', #15024, #8094, #305, .T. ) ;
#15401=( NAMED_UNIT ( * ) PLANE_ANGLE_UNIT ( ) SI_UNIT ( $, .RADIAN. ) );
#15415=CARTESIAN_POINT ( 'NONE',  ( -4.000000000000000000, -2.309401076758512694, -3.433295621305382461 ) ) ;
#15424=CARTESIAN_POINT ( 'NONE',  ( 0.000000000000000000, 0.000000000000000000, -4.974599999999998801 ) ) ;
#15436=EDGE_LOOP ( 'NONE', ( #18427, #4983 ) ) ;
#15437=CARTESIAN_POINT ( 'NONE',  ( 3.455068668934414777, -2.624017327439094327, -3.316620875263732504 ) ) ;
#15451=FACE_OUTER_BOUND ( 'NONE', #15936, .T. ) ;
#15505=EDGE_CURVE ( 'NONE', #19718, #18634, #6867, .T. ) ;
#15515=EDGE_CURVE ( 'NONE', #8094, #19958, #15119, .T. ) ;
#15524=CARTESIAN_POINT ( 'NONE',  ( -4.000000000000000000, 2.309401076758498483, -3.433295621305379353 ) ) ;
#15540=CARTESIAN_POINT ( 'NONE',  ( -6.259644161404860030E-16, -4.618802153517027165, -3.433295621305388234 ) ) ;
#15543=CARTESIAN_POINT ( 'NONE',  ( 4.000000000000003553, -2.309401076758513138, -3.504271511726786859 ) ) ;
#15555=( BOUNDED_SURFACE ( )  B_SPLINE_SURFACE ( 3, 2, ( 
 ( #7865, #11482, #9674 ),
 ( #540, #15187, #15311 ),
 ( #11715, #6304, #13393 ),
 ( #20660, #656, #13739 ),
 ( #18981, #4377, #4264 ),
 ( #11600, #22692, #7990 ) ),
 .UNSPECIFIED., .F., .F., .F. ) 
 B_SPLINE_SURFACE_WITH_KNOTS ( ( 4, 2, 4 ),
 ( 3, 3 ),
 ( 0.02032853247518125531, 0.02278863295364820865, 0.02524873343211516200 ),
 ( 0.000000000000000000, 1.000000000000000000 ),
 .UNSPECIFIED. ) 
 GEOMETRIC_REPRESENTATION_ITEM ( )  RATIONAL_B_SPLINE_SURFACE ( (
 ( 1.000000000000000000, 0.8047781615896836271, 1.000000000000000000),
 ( 1.000000000000000000, 0.8123767586289967202, 1.000000000000000000),
 ( 1.000000000000000000, 0.8190662415563443322, 1.000000000000000000),
 ( 1.000000000000000000, 0.8192361015669982205, 1.000000000000000000),
 ( 1.000000000000000000, 0.8126135807103181952, 1.000000000000000000),
 ( 1.000000000000000000, 0.8047712338318587788, 1.000000000000000000) ) ) 
 REPRESENTATION_ITEM ( '' )  SURFACE ( )  );
#15634=SURFACE_STYLE_USAGE ( .BOTH. , #4820 ) ;
#15656=CARTESIAN_POINT ( 'NONE',  ( 3.333333333333335702, -2.694301256218268215, -3.300726591567084256 ) ) ;
#15697=DIRECTION ( 'NONE',  ( 0.000000000000000000, 0.000000000000000000, -1.000000000000000000 ) ) ;
#15757=SHAPE_REPRESENTATION ( 'hex flange nut gradea_iso_ISO - 4161 - M5 - N', ( #7318 ), #16773 ) ;
#15760=ORIENTED_EDGE ( 'NONE', *, *, #12447, .T. ) ;
#15786=CARTESIAN_POINT ( 'NONE',  ( 3.453038570460273071, 2.625189405340834448, -3.535263753543585352 ) ) ;
#15798=DIRECTION ( 'NONE',  ( -0.000000000000000000, -0.000000000000000000, 1.000000000000000000 ) ) ;
#15840=ORIENTED_EDGE ( 'NONE', *, *, #20365, .F. ) ;
#15851=EDGE_CURVE ( 'NONE', #8889, #22700, #4283, .T. ) ;
#15880=SURFACE_STYLE_USAGE ( .BOTH. , #21347 ) ;
#15894=CARTESIAN_POINT ( 'NONE',  ( 2.742827927723449299, 3.035229711104609596, -3.433252694550591233 ) ) ;
#15923=CARTESIAN_POINT ( 'NONE',  ( -2.345747346278108214, 3.264484291692489215, -0.01223254789873409049 ) ) ;
#15936=EDGE_LOOP ( 'NONE', ( #15840, #11599 ) ) ;
#15951=CARTESIAN_POINT ( 'NONE',  ( -4.211140560182196957, -2.431303136016552013, -3.745885042887436178 ) ) ;
#15953=CARTESIAN_POINT ( 'NONE',  ( -4.000000000000000000, 0.000000000000000000, 0.000000000000000000 ) ) ;
#15971=AXIS2_PLACEMENT_3D ( 'NONE', #16375, #5943, #5466 ) ;
#16119=CARTESIAN_POINT ( 'NONE',  ( 0.000000000000000000, 0.000000000000000000, -25.03750572909317285 ) ) ;
#16186=DIRECTION ( 'NONE',  ( 0.9396926207859138680, 1.150791560227856926E-16, -0.3420201433256536139 ) ) ;
#16195=CARTESIAN_POINT ( 'NONE',  ( -4.207491450040567571, 2.029819825146470524, -3.671670828759566074 ) ) ;
#16228=CARTESIAN_POINT ( 'NONE',  ( 0.000000000000000000, 0.000000000000000000, 0.000000000000000000 ) ) ;
#16230=CARTESIAN_POINT ( 'NONE',  ( -4.000000000000000000, -1.942223658245633811, -0.3516579909967644246 ) ) ;
#16267=ORIENTED_EDGE ( 'NONE', *, *, #12877, .F. ) ;
#16304=VECTOR ( 'NONE', #7900, 1000.000000000000000 ) ;
#16324=VERTEX_POINT ( 'NONE', #17806 ) ;
#16341=DIRECTION ( 'NONE',  ( -0.000000000000000000, 0.000000000000000000, -1.000000000000000000 ) ) ;
#16353=ORIENTED_EDGE ( 'NONE', *, *, #3448, .T. ) ;
#16359=CARTESIAN_POINT ( 'NONE',  ( -2.100000000000000089, 2.571758278209441957E-16, -4.694516984716113228 ) ) ;
#16363=CONICAL_SURFACE ( 'NONE', #17131, 2.500000000000000888, 0.9599310885968785900 ) ;
#16365=PLANE ( 'NONE',  #13930 ) ;
#16375=CARTESIAN_POINT ( 'NONE',  ( 0.000000000000000000, 0.000000000000000000, -4.000000000000000000 ) ) ;
#16408=EDGE_LOOP ( 'NONE', ( #15760, #1891, #22709 ) ) ;
#16422=EDGE_CURVE ( 'NONE', #1978, #8665, #21014, .T. ) ;
#16453=AXIS2_PLACEMENT_3D ( 'NONE', #15424, #6299, #20878 ) ;
#16483=DIRECTION ( 'NONE',  ( -0.8660254037844377084, -0.5000000000000015543, 0.000000000000000000 ) ) ;
#16513=EDGE_CURVE ( 'NONE', #23289, #23683, #16854, .T. ) ;
#16519=ORIENTED_EDGE ( 'NONE', *, *, #22829, .F. ) ;
#16530=CARTESIAN_POINT ( 'NONE',  ( 3.349226789952652439, 2.685125164760731487, -0.2236248678334773199 ) ) ;
#16567=CARTESIAN_POINT ( 'NONE',  ( -4.203833317240879275, -1.627343821129593859, -3.597273115243890818 ) ) ;
#16630=CARTESIAN_POINT ( 'NONE',  ( 4.000000000000000000, -1.700175430507292473, -3.320327275037661785 ) ) ;
#16633=CARTESIAN_POINT ( 'NONE',  ( -4.197477534772231955, 0.8522413273724368521, -3.505042416683225692 ) ) ;
#16708=EDGE_CURVE ( 'NONE', #17879, #8889, #10293, .T. ) ;
#16767=CARTESIAN_POINT ( 'NONE',  ( 2.059999999999998721, 0.000000000000000000, -0.3080913168122742518 ) ) ;
#16773=( GEOMETRIC_REPRESENTATION_CONTEXT ( 3 ) GLOBAL_UNCERTAINTY_ASSIGNED_CONTEXT ( ( #16975 ) ) GLOBAL_UNIT_ASSIGNED_CONTEXT ( ( #15045, #15401, #3015 ) ) REPRESENTATION_CONTEXT ( 'NONE', 'WORKASPACE' ) );
#16781=CARTESIAN_POINT ( 'NONE',  ( 4.197393957002303999, -0.4069871074557456780, -3.503767560748925813 ) ) ;
#16783=PLANE ( 'NONE',  #23362 ) ;
#16789=VERTEX_POINT ( 'NONE', #17199 ) ;
#16815=EDGE_CURVE ( 'NONE', #9313, #17013, #13434, .T. ) ;
#16816=CARTESIAN_POINT ( 'NONE',  ( 1.567478505476135000E-15, 4.618802153517012954, -3.504269196027527844 ) ) ;
#16821=VERTEX_POINT ( 'NONE', #11177 ) ;
#16823=CARTESIAN_POINT ( 'NONE',  ( 0.1410422978106145031, -4.700232962125109104, -3.687027686973628704 ) ) ;
#16841=CARTESIAN_POINT ( 'NONE',  ( 1.734723475976807094E-15, 4.618802153517012954, -0.4999999999999995559 ) ) ;
#16854=B_SPLINE_CURVE_WITH_KNOTS ( 'NONE', 3,
 ( #17074, #648, #176, #11348, #13139, #16841 ),
 .UNSPECIFIED., .F., .F.,
 ( 4, 2, 4 ),
 ( 0.002365888236227977302, 0.003551327329835078910, 0.004736766423442180518 ),
 .UNSPECIFIED. ) ;
#16894=B_SPLINE_CURVE_WITH_KNOTS ( 'NONE', 3,
 ( #7755, #14830, #22084, #11118, #9557, #1976 ),
 .UNSPECIFIED., .F., .F.,
 ( 4, 2, 4 ),
 ( 0.002365888236227967761, 0.003551327329835077609, 0.004736766423442186590 ),
 .UNSPECIFIED. ) ;
#16915=ORIENTED_EDGE ( 'NONE', *, *, #16513, .F. ) ;
#16938=CARTESIAN_POINT ( 'NONE',  ( -0.5449313310646672903, -4.304185902836978883, -3.316620875263469159 ) ) ;
#16975=UNCERTAINTY_MEASURE_WITH_UNIT (LENGTH_MEASURE( 1.000000000000000082E-05 ), #15045, 'distance_accuracy_value', 'NONE');
#16977=EDGE_CURVE ( 'NONE', #21411, #8404, #6673, .T. ) ;
#17013=VERTEX_POINT ( 'NONE', #7920 ) ;
#17046=DIRECTION ( 'NONE',  ( 1.000000000000000000, 0.000000000000000000, 0.000000000000000000 ) ) ;
#17060=AXIS2_PLACEMENT_3D ( 'NONE', #10775, #5224, #10882 ) ;
#17062=ORIENTED_EDGE ( 'NONE', *, *, #4266, .F. ) ;
#17070=CARTESIAN_POINT ( 'NONE',  ( 1.567478505476134606E-15, 4.618802153517012066, -3.433295621305382905 ) ) ;
#17074=CARTESIAN_POINT ( 'NONE',  ( -2.000000000000006661, 3.464101615137750834, 0.000000000000000000 ) ) ;
#17108=ADVANCED_FACE ( 'NONE', ( #9841 ), #7473, .T. ) ;
#17131=AXIS2_PLACEMENT_3D ( 'NONE', #10309, #15697, #8609 ) ;
#17145=ORIENTED_EDGE ( 'NONE', *, *, #18327, .F. ) ;
#17173=ORIENTED_EDGE ( 'NONE', *, *, #3476, .T. ) ;
#17199=CARTESIAN_POINT ( 'NONE',  ( 4.000000000000000000, 2.309401076758515803, -0.4999999999999995559 ) ) ;
#17204=ORIENTED_EDGE ( 'NONE', *, *, #14521, .F. ) ;
#17208=CARTESIAN_POINT ( 'NONE',  ( 4.000000000000000000, 0.000000000000000000, 0.000000000000000000 ) ) ;
#17215=CARTESIAN_POINT ( 'NONE',  ( -1.144235203016679359, -3.958177651039096911, -0.09382832055446428676 ) ) ;
#17219=CARTESIAN_POINT ( 'NONE',  ( 2.807080416178989513, -3.225969019225150003, -3.502507215260505014 ) ) ;
#17240=ORIENTED_EDGE ( 'NONE', *, *, #6457, .F. ) ;
#17243=CARTESIAN_POINT ( 'NONE',  ( 2.000000000000008882, 3.464101615137749945, 0.000000000000000000 ) ) ;
#17258=CARTESIAN_POINT ( 'NONE',  ( -1.999999999999999556, 3.464101615137754830, -3.142992957459232795 ) ) ;
#17318=CARTESIAN_POINT ( 'NONE',  ( -4.211140560182196957, 2.431303136016537803, -3.745885042887433514 ) ) ;
#17323=FILL_AREA_STYLE_COLOUR ( '', #21781 ) ;
#17336=CARTESIAN_POINT ( 'NONE',  ( -0.02448733951239248641, -4.877042772274742255, -3.751161874094027571 ) ) ;
#17376=EDGE_LOOP ( 'NONE', ( #23488, #18884, #20418 ) ) ;
#17389=CARTESIAN_POINT ( 'NONE',  ( 0.000000000000000000, 0.000000000000000000, -4.974599999999998801 ) ) ;
#17404=CARTESIAN_POINT ( 'NONE',  ( 2.100000000000000089, 0.000000000000000000, -4.694516984716113228 ) ) ;
#17406=DIRECTION ( 'NONE',  ( -0.8191520442889902442, 0.000000000000000000, -0.5735764363510482688 ) ) ;
#17412=ORIENTED_EDGE ( 'NONE', *, *, #23195, .T. ) ;
#17441=CARTESIAN_POINT ( 'NONE',  ( 0.6666666666666658525, -4.233901974057276085, -3.300726591567086476 ) ) ;
#17451=ORIENTED_EDGE ( 'NONE', *, *, #3835, .F. ) ;
#17459=CARTESIAN_POINT ( 'NONE',  ( 1.390230914382191596, 4.043987460488659202, -3.502507215260488582 ) ) ;
#17508=ORIENTED_EDGE ( 'NONE', *, *, #10074, .T. ) ;
#17556=CARTESIAN_POINT ( 'NONE',  ( 1.999999999999998224, -3.464101615137772594, -3.142992957459239012 ) ) ;
#17568=CARTESIAN_POINT ( 'NONE',  ( -1.654252653721913102, -3.663718938583024443, -0.01223254789874440342 ) ) ;
#17572=CARTESIAN_POINT ( 'NONE',  ( -0.02511973781850462134, 4.877415612947412882, -3.751298745799839462 ) ) ;
#17587=EDGE_CURVE ( 'NONE', #1712, #5741, #4046, .T. ) ;
#17596=CARTESIAN_POINT ( 'NONE',  ( 0.3461262719736147297, -4.658553426539303821, -3.671615880910379381 ) ) ;
#17619=B_SPLINE_CURVE_WITH_KNOTS ( 'NONE', 3,
 ( #9281, #16567, #146, #7478 ),
 .UNSPECIFIED., .F., .F.,
 ( 4, 4 ),
 ( 0.000000000000000000, 0.002452478801916376308 ),
 .UNSPECIFIED. ) ;
#17622=EDGE_LOOP ( 'NONE', ( #4088, #22777, #14145, #10633 ) ) ;
#17630=DIRECTION ( 'NONE',  ( -0.000000000000000000, 0.000000000000000000, -1.000000000000000000 ) ) ;
#17636=DIRECTION ( 'NONE',  ( 1.000000000000000000, 0.000000000000000000, 0.000000000000000000 ) ) ;
#17676=CARTESIAN_POINT ( 'NONE',  ( -4.175002511812151873, -2.208363329454905877, -3.469254087858246738 ) ) ;
#17719=DIRECTION ( 'NONE',  ( -0.000000000000000000, 0.000000000000000000, -1.000000000000000000 ) ) ;
#17735=CARTESIAN_POINT ( 'NONE',  ( 0.000000000000000000, 0.000000000000000000, 0.000000000000000000 ) ) ;
#17806=CARTESIAN_POINT ( 'NONE',  ( 4.000000000000000000, 0.000000000000000000, 0.000000000000000000 ) ) ;
#17843=DIRECTION ( 'NONE',  ( 1.000000000000000000, 0.000000000000000000, 0.000000000000000000 ) ) ;
#17848=CARTESIAN_POINT ( 'NONE',  ( 2.687328764639642653, -3.067272167851299969, -0.05923475698271395140 ) ) ;
#17850=LINE ( 'NONE', #10813, #2894 ) ;
#17879=VERTEX_POINT ( 'NONE', #14595 ) ;
#17903=CARTESIAN_POINT ( 'NONE',  ( -3.540020015735593439, -2.810662092924100630, -3.602146406945814672 ) ) ;
#17908=ORIENTED_EDGE ( 'NONE', *, *, #2501, .F. ) ;
#18075=ORIENTED_EDGE ( 'NONE', *, *, #3448, .F. ) ;
#18096=DIRECTION ( 'NONE',  ( -1.000000000000000000, 0.000000000000000000, 0.000000000000000000 ) ) ;
#18147=CARTESIAN_POINT ( 'NONE',  ( 4.000000000000000000, 0.1981133338132474442, 2.382280164152719704E-17 ) ) ;
#18155=AXIS2_PLACEMENT_3D ( 'NONE', #15123, #713, #2625 ) ;
#18199=CARTESIAN_POINT ( 'NONE',  ( -5.384454397937118664, 6.702023979852544604E-16, -5.000000000000000000 ) ) ;
#18215=CARTESIAN_POINT ( 'NONE',  ( -1.240299975428113101E-15, -4.647091401871173311, -3.572172305156514849 ) ) ;
#18289=AXIS2_PLACEMENT_3D ( 'NONE', #20261, #2054, #11442 ) ;
#18295=DIRECTION ( 'NONE',  ( 1.224646799147353207E-16, 1.000000000000000000, 0.000000000000000000 ) ) ;
#18297=ORIENTED_EDGE ( 'NONE', *, *, #6457, .T. ) ;
#18314=VECTOR ( 'NONE', #880, 1000.000000000000000 ) ;
#18327=EDGE_CURVE ( 'NONE', #16821, #12663, #7112, .T. ) ;
#18337=CARTESIAN_POINT ( 'NONE',  ( 4.197393957002303999, 7.772902908466098641E-14, -3.503767560748929810 ) ) ;
#18373=CIRCLE ( 'NONE', #11522, 4.000000000000000000 ) ;
#18421=CARTESIAN_POINT ( 'NONE',  ( 4.000000000000000000, 1.680228229147133767, -3.316631783032546021 ) ) ;
#18423=DIRECTION ( 'NONE',  ( 0.8660254037844374864, -0.5000000000000018874, 0.000000000000000000 ) ) ;
#18426=DIRECTION ( 'NONE',  ( 0.000000000000000000, 0.000000000000000000, -1.000000000000000000 ) ) ;
#18427=ORIENTED_EDGE ( 'NONE', *, *, #15505, .T. ) ;
#18430=CARTESIAN_POINT ( 'NONE',  ( 1.411581201560190495E-15, 4.862606272033091592, -3.745885042887436622 ) ) ;
#18486=EDGE_CURVE ( 'NONE', #2584, #6221, #9800, .T. ) ;
#18534=CARTESIAN_POINT ( 'NONE',  ( 4.154306624731035846, -2.398490048085128556, -3.721999068284417955 ) ) ;
#18547=EDGE_LOOP ( 'NONE', ( #12131, #16353, #2159 ) ) ;
#18550=DIRECTION ( 'NONE',  ( 1.000000000000000000, 0.000000000000000000, 0.000000000000000000 ) ) ;
#18602=CARTESIAN_POINT ( 'NONE',  ( -0.6810597143197697489, -4.461075778259609770, -3.598441714920717516 ) ) ;
#18603=ORIENTED_EDGE ( 'NONE', *, *, #20957, .T. ) ;
#18633=EDGE_LOOP ( 'NONE', ( #2720, #9741, #1639, #8453 ) ) ;
#18634=VERTEX_POINT ( 'NONE', #298 ) ;
#18660=CARTESIAN_POINT ( 'NONE',  ( -4.000000000000000000, -0.8382240730041925492, -3.220610619767135141 ) ) ;
#18680=DIRECTION ( 'NONE',  ( -0.000000000000000000, -0.000000000000000000, 1.000000000000000000 ) ) ;
#18703=ORIENTED_EDGE ( 'NONE', *, *, #16977, .F. ) ;
#18740=DIRECTION ( 'NONE',  ( 0.000000000000000000, 0.000000000000000000, -1.000000000000000000 ) ) ;
#18758=FACE_OUTER_BOUND ( 'NONE', #12111, .T. ) ;
#18767=ORIENTED_EDGE ( 'NONE', *, *, #15505, .F. ) ;
#18791=CARTESIAN_POINT ( 'NONE',  ( -2.499999999999999556, 3.061616997868382648E-16, 3.469446951953614189E-15 ) ) ;
#18795=ORIENTED_EDGE ( 'NONE', *, *, #23292, .F. ) ;
#18853=LINE ( 'NONE', #9662, #18314 ) ;
#18876=CARTESIAN_POINT ( 'NONE',  ( 1.360585162435110629, -4.061296242128317857, -3.505054077164905024 ) ) ;
#18884=ORIENTED_EDGE ( 'NONE', *, *, #1261, .F. ) ;
#18891=ADVANCED_FACE ( 'NONE', ( #11954 ), #19223, .F. ) ;
#18899=CARTESIAN_POINT ( 'NONE',  ( -4.000000000000000000, 2.309401076758498483, -0.4999999999999927280 ) ) ;
#18921=AXIS2_PLACEMENT_3D ( 'NONE', #16119, #1599, #12180 ) ;
#18969=CARTESIAN_POINT ( 'NONE',  ( -4.101948962585905356, -2.368261337751088824, -3.681124513963624167 ) ) ;
#18981=CARTESIAN_POINT ( 'NONE',  ( -3.455068668934486276, 2.624017327439035707, -3.316620875263955437 ) ) ;
#18987=CARTESIAN_POINT ( 'NONE',  ( -0.3198814748697807464, -4.434118497892185040, -0.3507732604232532969 ) ) ;
#19004=CARTESIAN_POINT ( 'NONE',  ( 8.673617379884035472E-16, 4.618802153517012954, -5.000000000000000000 ) ) ;
#19038=ORIENTED_EDGE ( 'NONE', *, *, #20915, .T. ) ;
#19051=DIRECTION ( 'NONE',  ( 0.000000000000000000, 0.000000000000000000, -1.000000000000000000 ) ) ;
#19054=ADVANCED_FACE ( 'NONE', ( #10856 ), #7287, .F. ) ;
#19090=CARTESIAN_POINT ( 'NONE',  ( -5.560781378645573980, 0.000000000000000000, -4.000000000000000000 ) ) ;
#19102=CARTESIAN_POINT ( 'NONE',  ( 4.000000000000000000, -2.309401076758514915, -5.000000000000000000 ) ) ;
#19113=EDGE_LOOP ( 'NONE', ( #17908, #12342 ) ) ;
#19135=ORIENTED_EDGE ( 'NONE', *, *, #5989, .T. ) ;
#19139=LINE ( 'NONE', #10185, #16304 ) ;
#19173=DIRECTION ( 'NONE',  ( -1.000000000000000000, 0.000000000000000000, 0.000000000000000000 ) ) ;
#19223=CYLINDRICAL_SURFACE ( 'NONE', #18921, 2.500000000000000444 ) ;
#19225=CARTESIAN_POINT ( 'NONE',  ( 4.000000000000000000, -2.309401076758516691, -0.4999999999999995559 ) ) ;
#19243=DIRECTION ( 'NONE',  ( 0.000000000000000000, 0.000000000000000000, -1.000000000000000000 ) ) ;
#19248=CARTESIAN_POINT ( 'NONE',  ( 1.393927851585479161, -4.043713361053543842, -3.526374918436840922 ) ) ;
#19260=CARTESIAN_POINT ( 'NONE',  ( -2.000000000000002665, -3.464101615137770374, -3.142992957459237680 ) ) ;
#19262=ORIENTED_EDGE ( 'NONE', *, *, #13788, .T. ) ;
#19280=ORIENTED_EDGE ( 'NONE', *, *, #14986, .T. ) ;
#19310=VECTOR ( 'NONE', #11257, 999.9999999999998863 ) ;
#19312=ORIENTED_EDGE ( 'NONE', *, *, #19903, .T. ) ;
#19316=LINE ( 'NONE', #19090, #14457 ) ;
#19361=CARTESIAN_POINT ( 'NONE',  ( -6.473970235329672780E-16, -4.862606272033106691, -3.745885042887442395 ) ) ;
#19422=EDGE_LOOP ( 'NONE', ( #22446, #14663, #3566, #19262, #14182 ) ) ;
#19447=PRESENTATION_STYLE_ASSIGNMENT (( #15880 ) ) ;
#19465=CARTESIAN_POINT ( 'NONE',  ( 0.6810597143197052450, 4.461075778259290914, -3.598441714920602053 ) ) ;
#19498=CARTESIAN_POINT ( 'NONE',  ( -3.355112389629170799, 2.681727112203152963, -0.2256878752776689534 ) ) ;
#19517=DIRECTION ( 'NONE',  ( -1.000000000000000000, 0.000000000000000000, 0.000000000000000000 ) ) ;
#19519=CARTESIAN_POINT ( 'NONE',  ( 2.000000000000008882, 3.464101615137749945, 0.000000000000000000 ) ) ;
#19525=AXIS2_PLACEMENT_3D ( 'NONE', #7210, #14639, #14525 ) ;
#19530=CARTESIAN_POINT ( 'NONE',  ( -2.344047193898593395, -3.265465875126480455, -1.054683074273691752E-14 ) ) ;
#19544=( NAMED_UNIT ( * ) PLANE_ANGLE_UNIT ( ) SI_UNIT ( $, .RADIAN. ) );
#19577=UNCERTAINTY_MEASURE_WITH_UNIT (LENGTH_MEASURE( 1.000000000000000082E-05 ), #22806, 'distance_accuracy_value', 'NONE');
#19609=DIRECTION ( 'NONE',  ( -1.000000000000000000, 1.224646799147352714E-16, 0.000000000000000000 ) ) ;
#19637=CARTESIAN_POINT ( 'NONE',  ( -4.000000000000000000, 1.941961291383472732, -0.3515519931180205448 ) ) ;
#19640=EDGE_CURVE ( 'NONE', #23289, #8317, #4780, .T. ) ;
#19680=CARTESIAN_POINT ( 'NONE',  ( -4.140404888673278272, -2.228338276487456415, -3.686887068327035166 ) ) ;
#19718=VERTEX_POINT ( 'NONE', #20090 ) ;
#19747=CARTESIAN_POINT ( 'NONE',  ( -2.688821387764050996E-14, -4.618802153517012954, -0.4999999999999995559 ) ) ;
#19748=EDGE_CURVE ( 'NONE', #8094, #21424, #11489, .T. ) ;
#19758=FACE_OUTER_BOUND ( 'NONE', #16408, .T. ) ;
#19761=CARTESIAN_POINT ( 'NONE',  ( 0.000000000000000000, 0.000000000000000000, -4.000000000000000000 ) ) ;
#19798=DIRECTION ( 'NONE',  ( -1.000000000000000000, 0.000000000000000000, 0.000000000000000000 ) ) ;
#19802=CARTESIAN_POINT ( 'NONE',  ( -4.000000000000000000, 0.000000000000000000, 0.000000000000000000 ) ) ;
#19844=CARTESIAN_POINT ( 'NONE',  ( 4.000000000001088907, 1.658577278524410170, -3.531553309554541720 ) ) ;
#19849=FACE_OUTER_BOUND ( 'NONE', #6551, .T. ) ;
#19870=EDGE_LOOP ( 'NONE', ( #17412, #9466, #12275, #3723, #1397, #10432, #6063 ) ) ;
#19903=EDGE_CURVE ( 'NONE', #7467, #7989, #14921, .T. ) ;
#19930=ORIENTED_EDGE ( 'NONE', *, *, #21164, .T. ) ;
#19958=VERTEX_POINT ( 'NONE', #18899 ) ;
#20089=ORIENTED_EDGE ( 'NONE', *, *, #6663, .F. ) ;
#20090=CARTESIAN_POINT ( 'NONE',  ( 2.500000000000000444, 0.000000000000000000, -5.000000000000000888 ) ) ;
#20095=CARTESIAN_POINT ( 'NONE',  ( 3.999999999999999112, -1.539600717839012978, -3.300726591567080703 ) ) ;
#20153=AXIS2_PLACEMENT_3D ( 'NONE', #12289, #7444, #14758 ) ;
#20195=CARTESIAN_POINT ( 'NONE',  ( -0.3461262719736137305, 4.658553426539289610, -3.671615880910373608 ) ) ;
#20203=CARTESIAN_POINT ( 'NONE',  ( 4.000000000000000000, -2.511475576507276042, -3.469253905236643565 ) ) ;
#20205=CARTESIAN_POINT ( 'NONE',  ( -4.000000000000000000, -2.309401076758512694, -5.000000000000000000 ) ) ;
#20220=DIRECTION ( 'NONE',  ( 0.000000000000000000, 0.000000000000000000, -1.000000000000000000 ) ) ;
#20226=VECTOR ( 'NONE', #20464, 1000.000000000000000 ) ;
#20232=CARTESIAN_POINT ( 'NONE',  ( -6.473970235329672780E-16, -4.862606272033106691, -3.745885042887442395 ) ) ;
#20234=ADVANCED_FACE ( 'NONE', ( #276 ), #2502, .T. ) ;
#20261=CARTESIAN_POINT ( 'NONE',  ( 4.000000000000000000, 2.309401076758497151, -5.000000000000000000 ) ) ;
#20301=EDGE_CURVE ( 'NONE', #18634, #2584, #1834, .T. ) ;
#20365=EDGE_CURVE ( 'NONE', #5980, #5642, #22378, .T. ) ;
#20390=VERTEX_POINT ( 'NONE', #13594 ) ;
#20418=ORIENTED_EDGE ( 'NONE', *, *, #10465, .F. ) ;
#20422=AXIS2_PLACEMENT_3D ( 'NONE', #11144, #4045, #12823 ) ;
#20437=CARTESIAN_POINT ( 'NONE',  ( -2.059999999999998721, 2.522772406243545965E-16, -0.3080913168122742518 ) ) ;
#20443=EDGE_CURVE ( 'NONE', #19718, #6221, #10606, .T. ) ;
#20464=DIRECTION ( 'NONE',  ( 0.000000000000000000, 0.000000000000000000, 1.000000000000000000 ) ) ;
#20523=DIRECTION ( 'NONE',  ( -0.000000000000000000, -0.000000000000000000, 1.000000000000000000 ) ) ;
#20563=CARTESIAN_POINT ( 'NONE',  ( -4.000000000000000000, -2.512220745329312610, -3.469390707569719901 ) ) ;
#20568=CARTESIAN_POINT ( 'NONE',  ( 2.804994570502171047, 3.229033611042449792, -3.526374918436834704 ) ) ;
#20581=STYLED_ITEM ( 'NONE', ( #13838 ), #6193 ) ;
#20660=CARTESIAN_POINT ( 'NONE',  ( -2.725741868435985094, 3.045094352034055429, -3.220599429844047012 ) ) ;
#20710=ADVANCED_FACE ( 'NONE', ( #8176 ), #1731, .F. ) ;
#20753=DIRECTION ( 'NONE',  ( 0.000000000000000000, -1.000000000000000000, 0.000000000000000000 ) ) ;
#20770=CARTESIAN_POINT ( 'NONE',  ( 0.000000000000000000, 0.000000000000000000, 0.000000000000000000 ) ) ;
#20803=CARTESIAN_POINT ( 'NONE',  ( 4.211140560182196957, 2.431303136016536470, -3.745885042887433514 ) ) ;
#20858=VECTOR ( 'NONE', #7233, 1000.000000000000000 ) ;
#20878=DIRECTION ( 'NONE',  ( 1.000000000000000000, 0.000000000000000000, 0.000000000000000000 ) ) ;
#20886=ORIENTED_EDGE ( 'NONE', *, *, #22567, .F. ) ;
#20913=CARTESIAN_POINT ( 'NONE',  ( 5.384454397937118664, 0.000000000000000000, -5.000000000000000000 ) ) ;
#20915=EDGE_CURVE ( 'NONE', #21411, #3496, #17850, .T. ) ;
#20924=CARTESIAN_POINT ( 'NONE',  ( -2.171643655288372443, 3.365003104552320767, 2.541098841762897165E-18 ) ) ;
#20947=VERTEX_POINT ( 'NONE', #14030 ) ;
#20957=EDGE_CURVE ( 'NONE', #8889, #8094, #2699, .T. ) ;
#20972=SURFACE_STYLE_FILL_AREA ( #1098 ) ;
#21014=CIRCLE ( 'NONE', #13403, 2.100000000000000089 ) ;
#21029=EDGE_CURVE ( 'NONE', #8317, #16789, #6396, .T. ) ;
#21035=CARTESIAN_POINT ( 'NONE',  ( 4.211140560182196957, -2.431303136016555122, -3.745885042887436622 ) ) ;
#21109=CARTESIAN_POINT ( 'NONE',  ( -4.197393957002303999, 0.4069871074557429025, -3.503767560748926257 ) ) ;
#21144=DIRECTION ( 'NONE',  ( 0.000000000000000000, 0.000000000000000000, -1.000000000000000000 ) ) ;
#21149=CIRCLE ( 'NONE', #10515, 2.100000000000000089 ) ;
#21159=CARTESIAN_POINT ( 'NONE',  ( 0.000000000000000000, 0.000000000000000000, 0.000000000000000000 ) ) ;
#21164=EDGE_CURVE ( 'NONE', #21943, #7467, #3844, .T. ) ;
#21238=ORIENTED_EDGE ( 'NONE', *, *, #18327, .T. ) ;
#21304=CARTESIAN_POINT ( 'NONE',  ( -3.861362476283256129, -2.629030857716004199, -3.671615880910374941 ) ) ;
#21313=CARTESIAN_POINT ( 'NONE',  ( 4.203833317240879275, 1.627343821129582979, -3.597273115243889929 ) ) ;
#21330=ORIENTED_EDGE ( 'NONE', *, *, #13353, .T. ) ;
#21347=SURFACE_SIDE_STYLE ('',( #23157 ) ) ;
#21394=B_SPLINE_CURVE_WITH_KNOTS ( 'NONE', 3,
 ( #21780, #3115, #1299, #8639, #17848, #14516, #23219, #21537 ),
 .UNSPECIFIED., .F., .F.,
 ( 4, 2, 2, 4 ),
 ( 2.465131517071610173E-07, 0.001183067374689837636, 0.001774477805458902699, 0.002365888236227967761 ),
 .UNSPECIFIED. ) ;
#21411=VERTEX_POINT ( 'NONE', #6936 ) ;
#21424=VERTEX_POINT ( 'NONE', #22973 ) ;
#21429=CARTESIAN_POINT ( 'NONE',  ( -3.510273485745307287, -2.827716139362669967, -3.610536846335890004 ) ) ;
#21537=CARTESIAN_POINT ( 'NONE',  ( 2.000000000000005329, -3.464101615137751722, 0.000000000000000000 ) ) ;
#21539=CARTESIAN_POINT ( 'NONE',  ( -4.000000000000000000, 2.309401076758498483, -3.433295621305379353 ) ) ;
#21547=CARTESIAN_POINT ( 'NONE',  ( -0.6920835326022555245, -4.454600218803899558, -3.597382984111586079 ) ) ;
#21549=CARTESIAN_POINT ( 'NONE',  ( -4.000000000000000000, -2.309401076758515803, -0.4999999999999995559 ) ) ;
#21585=CARTESIAN_POINT ( 'NONE',  ( -4.000000000000000000, -0.7890432684750890990, -0.04868663549882315533 ) ) ;
#21665=FACE_OUTER_BOUND ( 'NONE', #8028, .T. ) ;
#21671=FACE_OUTER_BOUND ( 'NONE', #11355, .T. ) ;
#21673=CARTESIAN_POINT ( 'NONE',  ( 4.207491450040567571, -2.029819825146485179, -3.671670828759567407 ) ) ;
#21686=CARTESIAN_POINT ( 'NONE',  ( 2.500000000000000444, 0.000000000000000000, -25.03750572909317285 ) ) ;
#21687=EDGE_LOOP ( 'NONE', ( #10217, #11213, #21743, #9812, #8143 ) ) ;
#21693=ORIENTED_EDGE ( 'NONE', *, *, #4335, .T. ) ;
#21694=ADVANCED_FACE ( 'NONE', ( #9682 ), #5583, .F. ) ;
#21715=ORIENTED_EDGE ( 'NONE', *, *, #22539, .T. ) ;
#21741=CARTESIAN_POINT ( 'NONE',  ( 2.100000000000000089, 0.000000000000000000, -0.2800830152838844622 ) ) ;
#21743=ORIENTED_EDGE ( 'NONE', *, *, #23195, .F. ) ;
#21780=CARTESIAN_POINT ( 'NONE',  ( 4.000000000000000000, -2.309401076758516691, -0.4999999999999995559 ) ) ;
#21781=COLOUR_RGB ( '', 0.40784314, 0.44705882, 0.49803922) ;
#21852=ADVANCED_FACE ( 'NONE', ( #3296 ), #7141, .F. ) ;
#21858=ORIENTED_EDGE ( 'NONE', *, *, #14808, .F. ) ;
#21876=ORIENTED_EDGE ( 'NONE', *, *, #20915, .F. ) ;
#21883=CARTESIAN_POINT ( 'NONE',  ( 4.197310751797292738, 0.8178363989516252985, -3.502498386812444409 ) ) ;
#21884=ORIENTED_EDGE ( 'NONE', *, *, #1429, .T. ) ;
#21885=DIRECTION ( 'NONE',  ( 0.000000000000000000, 0.000000000000000000, 1.000000000000000000 ) ) ;
#21908=CARTESIAN_POINT ( 'NONE',  ( -1.240299975428134203E-15, -4.736529461165891242, -3.681130640444276292 ) ) ;
#21943=VERTEX_POINT ( 'NONE', #6780 ) ;
#21994=FACE_OUTER_BOUND ( 'NONE', #12513, .T. ) ;
#21999=DIRECTION ( 'NONE',  ( -0.5000000000000019984, -0.8660254037844375974, 0.000000000000000000 ) ) ;
#22000=CARTESIAN_POINT ( 'NONE',  ( -4.000000000000000000, 1.700094919196744270, -3.320312364301766017 ) ) ;
#22007=CARTESIAN_POINT ( 'NONE',  ( 0.6920835326022565237, 4.454600218803884459, -3.597382984111579862 ) ) ;
#22044=FACE_OUTER_BOUND ( 'NONE', #8159, .T. ) ;
#22061=LINE ( 'NONE', #1838, #1446 ) ;
#22084=CARTESIAN_POINT ( 'NONE',  ( 1.317756351988342622, -3.857995168970215438, -0.04852650426602527628 ) ) ;
#22096=ORIENTED_EDGE ( 'NONE', *, *, #16815, .T. ) ;
#22111=B_SPLINE_CURVE_WITH_KNOTS ( 'NONE', 3,
 ( #4383, #18987, #2816, #17215, #2928, #17568, #4742, #9919 ),
 .UNSPECIFIED., .F., .F.,
 ( 4, 2, 2, 4 ),
 ( 2.465131517390770070E-07, 0.001183067374689869946, 0.001774477805458935659, 0.002365888236228001588 ),
 .UNSPECIFIED. ) ;
#22141=CARTESIAN_POINT ( 'NONE',  ( 1.567478505476134606E-15, 4.618802153517012066, -3.433295621305382905 ) ) ;
#22176=CARTESIAN_POINT ( 'NONE',  ( 1.411581201560190495E-15, 4.862606272033091592, -3.745885042887436622 ) ) ;
#22179=CIRCLE ( 'NONE', #1535, 2.100000000000000089 ) ;
#22225=B_SPLINE_CURVE_WITH_KNOTS ( 'NONE', 3,
 ( #19225, #2812, #4140, #22811, #13507, #17208 ),
 .UNSPECIFIED., .F., .F.,
 ( 4, 2, 4 ),
 ( 0.003358874760055551890, 0.004541967308452098118, 0.005725059856848645212 ),
 .UNSPECIFIED. ) ;
#22242=CARTESIAN_POINT ( 'NONE',  ( 0.000000000000000000, 0.000000000000000000, 0.000000000000000000 ) ) ;
#22246=CARTESIAN_POINT ( 'NONE',  ( 1.734723475976807094E-15, 4.618802153517012954, -0.4999999999999995559 ) ) ;
#22261=CARTESIAN_POINT ( 'NONE',  ( -3.333333333333335258, 2.694301256218251783, -3.300726591567079815 ) ) ;
#22305=AXIS2_PLACEMENT_3D ( 'NONE', #13916, #6955, #9001 ) ;
#22378=CIRCLE ( 'NONE', #23151, 5.384454397937118664 ) ;
#22438=DIRECTION ( 'NONE',  ( -1.000000000000000000, 0.000000000000000000, 0.000000000000000000 ) ) ;
#22443=MANIFOLD_SOLID_BREP ( 'EndChamfer', #14314 ) ;
#22446=ORIENTED_EDGE ( 'NONE', *, *, #15053, .F. ) ;
#22454=B_SPLINE_CURVE_WITH_KNOTS ( 'NONE', 3,
 ( #8905, #21313, #4936, #23243 ),
 .UNSPECIFIED., .F., .F.,
 ( 4, 4 ),
 ( 0.000000000000000000, 0.002452478801916361129 ),
 .UNSPECIFIED. ) ;
#22533=EDGE_CURVE ( 'NONE', #6221, #2584, #15326, .T. ) ;
#22539=EDGE_CURVE ( 'NONE', #21943, #14331, #10148, .T. ) ;
#22567=EDGE_CURVE ( 'NONE', #7262, #10320, #1900, .T. ) ;
#22592=CARTESIAN_POINT ( 'NONE',  ( 4.175648173966055587, -2.207990556236547608, -3.469390959564065291 ) ) ;
#22622=ORIENTED_EDGE ( 'NONE', *, *, #16422, .T. ) ;
#22627=DIRECTION ( 'NONE',  ( 0.000000000000000000, -0.000000000000000000, 1.000000000000000000 ) ) ;
#22663=EDGE_LOOP ( 'NONE', ( #8514, #3775, #2011, #10682 ) ) ;
#22670=DIRECTION ( 'NONE',  ( -1.000000000000000000, 0.000000000000000000, 0.000000000000000000 ) ) ;
#22692=CARTESIAN_POINT ( 'NONE',  ( -4.141042297810615835, 2.227970268150415656, -3.687027686973619822 ) ) ;
#22700=VERTEX_POINT ( 'NONE', #1708 ) ;
#22709=ORIENTED_EDGE ( 'NONE', *, *, #3476, .F. ) ;
#22723=CARTESIAN_POINT ( 'NONE',  ( 4.154306624731137099, 2.398490048084935822, -3.721999068284414847 ) ) ;
#22726=CONICAL_SURFACE ( 'NONE', #20422, 2.059999999999998721, 0.9599310885968738161 ) ;
#22777=ORIENTED_EDGE ( 'NONE', *, *, #6663, .T. ) ;
#22790=CARTESIAN_POINT ( 'NONE',  ( 2.000000000000008882, 3.464101615137749945, 0.000000000000000000 ) ) ;
#22806=( LENGTH_UNIT ( ) NAMED_UNIT ( * ) SI_UNIT ( .MILLI., .METRE. ) );
#22808=CARTESIAN_POINT ( 'NONE',  ( 4.211140560182196957, -2.431303136016555122, -3.745885042887436622 ) ) ;
#22811=CARTESIAN_POINT ( 'NONE',  ( 3.999999999999999112, -0.7890432684750902093, -0.04868663549882291247 ) ) ;
#22818=CARTESIAN_POINT ( 'NONE',  ( 2.756197834950227410, 3.027510591568626896, -3.223146290109805356 ) ) ;
#22829=EDGE_CURVE ( 'NONE', #7467, #15024, #2895, .T. ) ;
#22857=AXIS2_PLACEMENT_3D ( 'NONE', #14997, #4057, #8795 ) ;
#22904=CIRCLE ( 'NONE', #23678, 5.560781378645573980 ) ;
#22925=CARTESIAN_POINT ( 'NONE',  ( -4.197393957002303999, -7.773935952363655451E-14, -3.503767560748929810 ) ) ;
#22928=CARTESIAN_POINT ( 'NONE',  ( 4.000000000000000000, -2.309401076758514915, -3.433295621305383349 ) ) ;
#22945=CARTESIAN_POINT ( 'NONE',  ( 4.175002511812151873, 2.208363329454889445, -3.469254087858244073 ) ) ;
#22973=CARTESIAN_POINT ( 'NONE',  ( -4.000000000000000000, -2.309401076758512694, -3.433295621305382461 ) ) ;
#22980=CARTESIAN_POINT ( 'NONE',  ( -6.259644161404860030E-16, -4.618802153517027165, -3.433295621305388234 ) ) ;
#23057=CARTESIAN_POINT ( 'NONE',  ( 0.5636800770130377947, 4.293361309317166530, -3.531542292954102713 ) ) ;
#23099=CARTESIAN_POINT ( 'NONE',  ( -2.500000000000000888, 0.000000000000000000, -4.974599999999998801 ) ) ;
#23120=CARTESIAN_POINT ( 'NONE',  ( -2.000000000000007550, -3.464101615137749945, 0.000000000000000000 ) ) ;
#23134=SHAPE_REPRESENTATION_RELATIONSHIP ( 'NONE' , 'NONE' ,  #15757, #6193 ) ;
#23139=ORIENTED_EDGE ( 'NONE', *, *, #1173, .F. ) ;
#23151=AXIS2_PLACEMENT_3D ( 'NONE', #7734, #15050, #632 ) ;
#23157=SURFACE_STYLE_FILL_AREA ( #2807 ) ;
#23195=EDGE_CURVE ( 'NONE', #7989, #9313, #22454, .T. ) ;
#23219=CARTESIAN_POINT ( 'NONE',  ( 2.171643655288379993, -3.365003104552334978, -1.195831703456429434E-14 ) ) ;
#23225=CARTESIAN_POINT ( 'NONE',  ( 4.000000000000000000, -2.309401076758516691, -0.4999999999999995559 ) ) ;
#23243=CARTESIAN_POINT ( 'NONE',  ( 4.197393957002303999, 7.772902908466098641E-14, -3.503767560748929810 ) ) ;
#23289=VERTEX_POINT ( 'NONE', #9487 ) ;
#23292=EDGE_CURVE ( 'NONE', #20947, #7262, #18373, .T. ) ;
#23294=ORIENTED_EDGE ( 'NONE', *, *, #16422, .F. ) ;
#23362=AXIS2_PLACEMENT_3D ( 'NONE', #15125, #19798, #10745 ) ;
#23403=CARTESIAN_POINT ( 'NONE',  ( -2.836893136758495970, -3.208949435745868328, -3.505054077164885484 ) ) ;
#23434=DIRECTION ( 'NONE',  ( 1.000000000000000000, 0.000000000000000000, 0.000000000000000000 ) ) ;
#23488=ORIENTED_EDGE ( 'NONE', *, *, #22567, .T. ) ;
#23528=( BOUNDED_SURFACE ( )  B_SPLINE_SURFACE ( 3, 2, ( 
 ( #459, #14740, #334 ),
 ( #22000, #5613, #11150 ),
 ( #9700, #9345, #16633 ),
 ( #18660, #211, #7542 ),
 ( #2247, #2368, #3925 ),
 ( #20563, #7668, #14861 ) ),
 .UNSPECIFIED., .F., .F., .F. ) 
 B_SPLINE_SURFACE_WITH_KNOTS ( ( 4, 2, 4 ),
 ( 3, 3 ),
 ( 0.02027752710269158445, 0.02273781595091097299, 0.02519810479913036153 ),
 ( 0.000000000000000000, 1.000000000000000000 ),
 .UNSPECIFIED. ) 
 GEOMETRIC_REPRESENTATION_ITEM ( )  RATIONAL_B_SPLINE_SURFACE ( (
 ( 1.000000000000000000, 0.8047781431712808242, 1.000000000000000000),
 ( 1.000000000000000000, 0.8123773247083928561, 1.000000000000000000),
 ( 1.000000000000000000, 0.8190670192154906326, 1.000000000000000000),
 ( 1.000000000000000000, 0.8192353552912178261, 1.000000000000000000),
 ( 1.000000000000000000, 0.8126132098226825917, 1.000000000000000000),
 ( 1.000000000000000000, 0.8047712465856394770, 1.000000000000000000) ) ) 
 REPRESENTATION_ITEM ( '' )  SURFACE ( )  );
#23600=CARTESIAN_POINT ( 'NONE',  ( -2.449848172108560540, -3.432307619358754724, -3.503702292528910078 ) ) ;
#23628=AXIS2_PLACEMENT_3D ( 'NONE', #21159, #17719, #6813 ) ;
#23674=ORIENTED_EDGE ( 'NONE', *, *, #22533, .T. ) ;
#23678=AXIS2_PLACEMENT_3D ( 'NONE', #19761, #10353, #8541 ) ;
#23683=VERTEX_POINT ( 'NONE', #8525 ) ;
ENDSEC;
END-ISO-10303-21;
